ISO-10303-21;
HEADER;
FILE_DESCRIPTION (('STEP AP214'),
    '1' );
FILE_NAME ('hex thin nut chamfered gradeab_iso_ISO - 4035 - M36 - N.step',
    '2026-10-08T07:58:12',
    ( '' ),
    ( '' ),
    'SwSTEP 2.0',
    'SolidWorks 2026',
    '' );
FILE_SCHEMA (( 'AUTOMOTIVE_DESIGN' ));
ENDSEC;

DATA;
#23=LINE ( 'NONE', #2905, #21261 ) ;
#27=ADVANCED_FACE ( 'NONE', ( #25458 ), #22740, .T. ) ;
#44=ORIENTED_EDGE ( 'NONE', *, *, #27793, .F. ) ;
#62=CARTESIAN_POINT ( 'NONE',  ( -27.49999999999999645, -5.348566131067992835, -0.2306174136865311308 ) ) ;
#97=CARTESIAN_POINT ( 'NONE',  ( 27.50000000000001066, -2.682974265912531742, -6.098637220230963674E-17 ) ) ;
#131=ORIENTED_EDGE ( 'NONE', *, *, #28510, .T. ) ;
#204=ORIENTED_EDGE ( 'NONE', *, *, #10925, .T. ) ;
#209=CARTESIAN_POINT ( 'NONE',  ( 11.41286821541921803, -25.16504226903143149, -17.92845254598169902 ) ) ;
#253=VERTEX_POINT ( 'NONE', #11433 ) ;
#263=COLOUR_RGB ( '', 0.31764706, 0.68627451, 0.89019608) ;
#355=VERTEX_POINT ( 'NONE', #16197 ) ;
#361=ADVANCED_FACE ( 'NONE', ( #27937 ), #11271, .T. ) ;
#395=EDGE_CURVE ( 'NONE', #7505, #355, #22318, .T. ) ;
#459=DIRECTION ( 'NONE',  ( 0.000000000000000000, -0.000000000000000000, 1.000000000000000000 ) ) ;
#493=ORIENTED_EDGE ( 'NONE', *, *, #9737, .T. ) ;
#496=VECTOR ( 'NONE', #27599, 1000.000000000000000 ) ;
#542=AXIS2_PLACEMENT_3D ( 'NONE', #1520, #30308, #26911 ) ;
#817=ORIENTED_EDGE ( 'NONE', *, *, #26586, .F. ) ;
#902=AXIS2_PLACEMENT_3D ( 'NONE', #9614, #1446, #27504 ) ;
#944=ORIENTED_EDGE ( 'NONE', *, *, #7946, .F. ) ;
#980=FACE_OUTER_BOUND ( 'NONE', #1402, .T. ) ;
#993=AXIS2_PLACEMENT_3D ( 'NONE', #19471, #32747, #14366 ) ;
#1008=AXIS2_PLACEMENT_3D ( 'NONE', #4742, #5084, #30817 ) ;
#1020=CARTESIAN_POINT ( 'NONE',  ( 2.249320974685019792, 30.45561873520115270, -16.29357272760982411 ) ) ;
#1080=CARTESIAN_POINT ( 'NONE',  ( -14.33345751131668955, -23.47883925285270834, -17.99999999999999645 ) ) ;
#1105=CARTESIAN_POINT ( 'NONE',  ( 0.000000000000000000, 0.000000000000000000, -18.00000000000000000 ) ) ;
#1117=CARTESIAN_POINT ( 'NONE',  ( 27.50000000000000355, 15.87713240271469317, -18.00000000000000000 ) ) ;
#1178=DIRECTION ( 'NONE',  ( -0.000000000000000000, -0.000000000000000000, 1.000000000000000000 ) ) ;
#1183=EDGE_LOOP ( 'NONE', ( #6771, #131, #30193, #14259, #7403, #30165 ) ) ;
#1196=ADVANCED_FACE ( 'NONE', ( #25855 ), #12953, .T. ) ;
#1218=CARTESIAN_POINT ( 'NONE',  ( 27.50000000000001066, -2.682974265912535294, -18.00000000000000355 ) ) ;
#1258=CONICAL_SURFACE ( 'NONE', #22487, 27.50000000000000355, 1.047197551196595411 ) ;
#1298=CARTESIAN_POINT ( 'NONE',  ( 18.40606158072673537, -21.12752019707603779, -17.76591125084755163 ) ) ;
#1322=SURFACE_STYLE_FILL_AREA ( #6767 ) ;
#1395=DIRECTION ( 'NONE',  ( -0.000000000000000000, -0.000000000000000000, 1.000000000000000000 ) ) ;
#1402=EDGE_LOOP ( 'NONE', ( #32485, #23415, #19645, #30569 ) ) ;
#1415=EDGE_LOOP ( 'NONE', ( #27587, #28020, #15988, #9582, #29643, #3118 ) ) ;
#1425=CARTESIAN_POINT ( 'NONE',  ( -16.00000000000000000, 1.959434878635765131E-15, -18.00000000000000000 ) ) ;
#1446=DIRECTION ( 'NONE',  ( -0.5000000000000004441, -0.8660254037844383745, 0.000000000000000000 ) ) ;
#1458=CARTESIAN_POINT ( 'NONE',  ( 16.09259079475562615, -22.46320317811879264, -17.99999999999998579 ) ) ;
#1520=CARTESIAN_POINT ( 'NONE',  ( -6.938893903907228378E-15, 31.75426480542944319, 0.000000000000000000 ) ) ;
#1553=CARTESIAN_POINT ( 'NONE',  ( -9.093938419273312590, -26.50387701106812344, -0.2340887491524524799 ) ) ;
#1556=AXIS2_PLACEMENT_3D ( 'NONE', #24295, #8307, #8795 ) ;
#1608=ORIENTED_EDGE ( 'NONE', *, *, #24349, .F. ) ;
#1618=DIRECTION ( 'NONE',  ( -0.8660254037844381525, 0.5000000000000007772, 0.000000000000000000 ) ) ;
#1634=CARTESIAN_POINT ( 'NONE',  ( 27.49999999999999645, 5.390523180938858516, -17.71625836475401172 ) ) ;
#1640=B_SPLINE_CURVE_WITH_KNOTS ( 'NONE', 3,
 ( #8047, #14729, #17630, #26259, #20182, #22572 ),
 .UNSPECIFIED., .F., .F.,
 ( 4, 2, 4 ),
 ( 2.380727409349380532E-07, 0.008032766472079795605, 0.01606529487141865678 ),
 .UNSPECIFIED. ) ;
#1774=CARTESIAN_POINT ( 'NONE',  ( -27.50000000000000000, -13.28298644054430611, -16.25870334244831383 ) ) ;
#1785=VERTEX_POINT ( 'NONE', #28376 ) ;
#1794=CIRCLE ( 'NONE', #11597, 18.00000000000000711 ) ;
#1800=CARTESIAN_POINT ( 'NONE',  ( -27.50000000000000000, 15.87713240271469672, -18.00000000000000000 ) ) ;
#1865=ADVANCED_FACE ( 'NONE', ( #6145 ), #11765, .F. ) ;
#1901=EDGE_CURVE ( 'NONE', #253, #21688, #5459, .T. ) ;
#1945=B_SPLINE_CURVE_WITH_KNOTS ( 'NONE', 3,
 ( #9290, #30425, #17302, #1298, #1458, #19684 ),
 .UNSPECIFIED., .F., .F.,
 ( 4, 2, 4 ),
 ( 2.380727408830323507E-07, 0.008032766472079741829, 0.01606529487141860127 ),
 .UNSPECIFIED. ) ;
#2000=B_SPLINE_CURVE_WITH_KNOTS ( 'NONE', 3,
 ( #18159, #23925, #28554, #15585, #26152, #13043, #97, #10498 ),
 .UNSPECIFIED., .F., .F.,
 ( 4, 2, 2, 4 ),
 ( 0.02832689070575901413, 0.03234239231761928957, 0.03635789392947956500, 0.04438889715320012974 ),
 .UNSPECIFIED. ) ;
#2001=CONICAL_SURFACE ( 'NONE', #14490, 27.50000000000000355, 1.047197551196595411 ) ;
#2122=ORIENTED_EDGE ( 'NONE', *, *, #9157, .F. ) ;
#2152=DIRECTION ( 'NONE',  ( 0.000000000000000000, 0.000000000000000000, 1.000000000000000000 ) ) ;
#2213=EDGE_LOOP ( 'NONE', ( #7834, #204, #21981, #13188, #17457, #11834 ) ) ;
#2272=CARTESIAN_POINT ( 'NONE',  ( -16.66875746037183248, -22.13055319862718662, -0.1142222407377356808 ) ) ;
#2275=FACE_OUTER_BOUND ( 'NONE', #6180, .T. ) ;
#2291=AXIS2_PLACEMENT_3D ( 'NONE', #19859, #12199, #22586 ) ;
#2296=ADVANCED_FACE ( 'NONE', ( #32885 ), #29338, .T. ) ;
#2334=EDGE_CURVE ( 'NONE', #23864, #8655, #27770, .T. ) ;
#2352=DIRECTION ( 'NONE',  ( 0.000000000000000000, 0.000000000000000000, 1.000000000000000000 ) ) ;
#2371=CONICAL_SURFACE ( 'NONE', #22466, 27.50000000000000355, 1.047197551196595411 ) ;
#2404=AXIS2_PLACEMENT_3D ( 'NONE', #8872, #11941, #4266 ) ;
#2420=B_SPLINE_CURVE_WITH_KNOTS ( 'NONE', 3,
 ( #16033, #31218, #15368, #209, #28493, #12988, #5645, #23703, #25760, #26260 ),
 .UNSPECIFIED., .F., .F.,
 ( 4, 2, 2, 2, 4 ),
 ( 0.01606529487141860127, 0.01806591702017404377, 0.02006653916892948628, 0.02406778346644037475, 0.03207027206146215170 ),
 .UNSPECIFIED. ) ;
#2425=ORIENTED_EDGE ( 'NONE', *, *, #11054, .T. ) ;
#2454=CARTESIAN_POINT ( 'NONE',  ( 27.50000000000000711, 10.70896984529284879, -1.097913889158304235 ) ) ;
#2468=EDGE_LOOP ( 'NONE', ( #21190, #44, #10482, #2924, #29269, #18804 ) ) ;
#2578=CARTESIAN_POINT ( 'NONE',  ( -25.25067902531498376, 17.17577847294296234, -16.29357272760983477 ) ) ;
#2621=CARTESIAN_POINT ( 'NONE',  ( -27.50000000000000000, 13.30988860919478078, -1.715101482986570502 ) ) ;
#2694=EDGE_CURVE ( 'NONE', #23832, #31784, #22331, .T. ) ;
#2698=ORIENTED_EDGE ( 'NONE', *, *, #15203, .T. ) ;
#2826=DIRECTION ( 'NONE',  ( 1.000000000000000000, 0.000000000000000000, 0.000000000000000000 ) ) ;
#2905=CARTESIAN_POINT ( 'NONE',  ( 18.00000000000000711, 2.204364238465236217E-15, -17.97459999999999525 ) ) ;
#2924=ORIENTED_EDGE ( 'NONE', *, *, #13743, .T. ) ;
#2950=DIRECTION ( 'NONE',  ( 0.000000000000000000, -0.000000000000000000, 1.000000000000000000 ) ) ;
#2959=DIRECTION ( 'NONE',  ( -0.000000000000000000, 0.000000000000000000, -1.000000000000000000 ) ) ;
#3049=EDGE_LOOP ( 'NONE', ( #9531, #9267, #20394 ) ) ;
#3064=DIRECTION ( 'NONE',  ( 1.000000000000000000, 0.000000000000000000, 0.000000000000000000 ) ) ;
#3118=ORIENTED_EDGE ( 'NONE', *, *, #17655, .F. ) ;
#3124=ORIENTED_EDGE ( 'NONE', *, *, #17926, .F. ) ;
#3176=UNCERTAINTY_MEASURE_WITH_UNIT (LENGTH_MEASURE( 1.000000000000000082E-05 ), #18194, 'distance_accuracy_value', 'NONE');
#3246=ORIENTED_EDGE ( 'NONE', *, *, #26650, .T. ) ;
#3288=ORIENTED_EDGE ( 'NONE', *, *, #2694, .T. ) ;
#3290=CARTESIAN_POINT ( 'NONE',  ( -18.40782811468576341, -21.12650028821926185, -17.71727689882191470 ) ) ;
#3340=CARTESIAN_POINT ( 'NONE',  ( 4.515071337844623223, 29.14748715311447924, -1.088725517910807294 ) ) ;
#3348=CARTESIAN_POINT ( 'NONE',  ( -27.50000000000000711, 10.70896984529285767, -16.90208611084169732 ) ) ;
#3399=CARTESIAN_POINT ( 'NONE',  ( -10.83124253962820305, 25.50084400951695329, -17.88577775926227886 ) ) ;
#3473=DIRECTION ( 'NONE',  ( -0.000000000000000000, -0.000000000000000000, 1.000000000000000000 ) ) ;
#3633=DIRECTION ( 'NONE',  ( -0.000000000000000000, -0.000000000000000000, 1.000000000000000000 ) ) ;
#3635=EDGE_CURVE ( 'NONE', #22495, #26131, #8923, .T. ) ;
#3639=DIRECTION ( 'NONE',  ( 0.000000000000000000, 0.000000000000000000, 1.000000000000000000 ) ) ;
#3740=CARTESIAN_POINT ( 'NONE',  ( 11.40740920524441115, 25.16819403002534727, -18.00000000000000000 ) ) ;
#3770=CARTESIAN_POINT ( 'NONE',  ( -25.25067902531499442, 17.17577847294295523, -1.706427272390161454 ) ) ;
#3817=EDGE_LOOP ( 'NONE', ( #15149, #11920, #30667 ) ) ;
#3852=DIRECTION ( 'NONE',  ( -1.000000000000000000, 3.552713678800500929E-15, 0.000000000000000000 ) ) ;
#3907=ADVANCED_FACE ( 'NONE', ( #2275 ), #26203, .T. ) ;
#3949=DIRECTION ( 'NONE',  ( -0.8660254037844382635, -0.5000000000000006661, 0.000000000000000000 ) ) ;
#3972=EDGE_CURVE ( 'NONE', #12567, #1785, #23202, .T. ) ;
#3989=CARTESIAN_POINT ( 'NONE',  ( -11.41286821541921626, 25.16504226903141372, -0.07154745401828305207 ) ) ;
#4072=CARTESIAN_POINT ( 'NONE',  ( 9.093938419273300156, 26.50387701106810923, -17.76591125084756229 ) ) ;
#4103=DIRECTION ( 'NONE',  ( -1.000000000000000000, 0.000000000000000000, 0.000000000000000000 ) ) ;
#4121=EDGE_CURVE ( 'NONE', #31784, #8655, #17522, .T. ) ;
#4127=EDGE_CURVE ( 'NONE', #6898, #26498, #22379, .T. ) ;
#4148=ORIENTED_EDGE ( 'NONE', *, *, #33090, .T. ) ;
#4149=CARTESIAN_POINT ( 'NONE',  ( -2.243702833038399902, 30.45886237079319514, -1.708299986272438842 ) ) ;
#4201=DIRECTION ( 'NONE',  ( 1.000000000000000000, 0.000000000000000000, 0.000000000000000000 ) ) ;
#4212=DIRECTION ( 'NONE',  ( 1.000000000000000000, 0.000000000000000000, 0.000000000000000000 ) ) ;
#4266=DIRECTION ( 'NONE',  ( 1.000000000000000000, 0.000000000000000000, 0.000000000000000000 ) ) ;
#4267=CARTESIAN_POINT ( 'NONE',  ( 0.000000000000000000, 0.000000000000000000, 0.000000000000000000 ) ) ;
#4321=DIRECTION ( 'NONE',  ( 0.000000000000000000, 0.000000000000000000, 1.000000000000000000 ) ) ;
#4338=CARTESIAN_POINT ( 'NONE',  ( -27.50000000000000711, -9.324699302609172236, -17.12819780694306004 ) ) ;
#4528=EDGE_CURVE ( 'NONE', #21688, #31784, #28925, .T. ) ;
#4551=DIRECTION ( 'NONE',  ( -1.000000000000000000, 0.000000000000000000, 0.000000000000000000 ) ) ;
#4614=( GEOMETRIC_REPRESENTATION_CONTEXT ( 3 ) GLOBAL_UNCERTAINTY_ASSIGNED_CONTEXT ( ( #21276 ) ) GLOBAL_UNIT_ASSIGNED_CONTEXT ( ( #26679, #5566, #10693 ) ) REPRESENTATION_CONTEXT ( 'NONE', 'WORKASPACE' ) );
#4615=CARTESIAN_POINT ( 'NONE',  ( 27.50000000000000355, 15.87713240271469317, -18.00000000000000000 ) ) ;
#4742=CARTESIAN_POINT ( 'NONE',  ( 0.000000000000000000, 0.000000000000000000, -25.03750572909317285 ) ) ;
#4763=CARTESIAN_POINT ( 'NONE',  ( 18.00000000000000711, 2.204364238465236217E-15, -17.97459999999999525 ) ) ;
#4787=CARTESIAN_POINT ( 'NONE',  ( 18.40606158072673182, -21.12752019707603424, -0.2340887491524535069 ) ) ;
#4813=EDGE_LOOP ( 'NONE', ( #8074, #7187, #7163, #16722 ) ) ;
#4832=EDGE_CURVE ( 'NONE', #32368, #8582, #22968, .T. ) ;
#4845=CARTESIAN_POINT ( 'NONE',  ( 10.83124253962820305, -25.50084400951698527, -0.1142222407377387061 ) ) ;
#4858=ORIENTED_EDGE ( 'NONE', *, *, #4975, .F. ) ;
#4888=EDGE_LOOP ( 'NONE', ( #8453, #28571, #8129 ) ) ;
#4897=DIRECTION ( 'NONE',  ( -1.000000000000000000, 0.000000000000000000, 0.000000000000000000 ) ) ;
#4903=CYLINDRICAL_SURFACE ( 'NONE', #5306, 16.00000000000000000 ) ;
#4939=EDGE_LOOP ( 'NONE', ( #20400, #17543, #13634, #16072 ) ) ;
#4975=EDGE_CURVE ( 'NONE', #8265, #26498, #11011, .T. ) ;
#5018=EDGE_CURVE ( 'NONE', #17155, #25250, #23, .T. ) ;
#5084=DIRECTION ( 'NONE',  ( -0.000000000000000000, -0.000000000000000000, 1.000000000000000000 ) ) ;
#5114=FACE_OUTER_BOUND ( 'NONE', #22649, .T. ) ;
#5164=CARTESIAN_POINT ( 'NONE',  ( 13.75000000000002487, 23.81569860407205397, 0.000000000000000000 ) ) ;
#5166=CARTESIAN_POINT ( 'NONE',  ( -27.50000000000000000, 15.87713240271469672, -2.456200930618631428 ) ) ;
#5180=CARTESIAN_POINT ( 'NONE',  ( 2.243702833038385247, -30.45886237079320580, -1.708299986272457938 ) ) ;
#5306=AXIS2_PLACEMENT_3D ( 'NONE', #15289, #2352, #23133 ) ;
#5311=AXIS2_PLACEMENT_3D ( 'NONE', #7275, #18002, #33333 ) ;
#5328=CARTESIAN_POINT ( 'NONE',  ( 14.91983402814537563, 23.14029461301514345, -0.01440555954223494972 ) ) ;
#5457=CARTESIAN_POINT ( 'NONE',  ( -27.50000000000000000, -15.87713240271474824, -2.456200930618646971 ) ) ;
#5459=B_SPLINE_CURVE_WITH_KNOTS ( 'NONE', 3,
 ( #32209, #3770, #11440, #9217, #22155, #6496 ),
 .UNSPECIFIED., .F., .F.,
 ( 4, 2, 4 ),
 ( 2.380727408877235103E-07, 0.008032766472079745299, 0.01606529487141860474 ),
 .UNSPECIFIED. ) ;
#5518=DIRECTION ( 'NONE',  ( 1.000000000000000000, 0.000000000000000000, 0.000000000000000000 ) ) ;
#5566=( NAMED_UNIT ( * ) PLANE_ANGLE_UNIT ( ) SI_UNIT ( $, .RADIAN. ) );
#5645=CARTESIAN_POINT ( 'NONE',  ( 7.940546747334011890, -27.16978800334334565, -17.55088044235630562 ) ) ;
#5699=CARTESIAN_POINT ( 'NONE',  ( 18.00000000000000355, 0.000000000000000000, -18.00000000000000000 ) ) ;
#5748=EDGE_CURVE ( 'NONE', #28277, #6898, #21106, .T. ) ;
#5821=CARTESIAN_POINT ( 'NONE',  ( 27.50000000000001066, -15.87713240271473580, -15.54379906938135214 ) ) ;
#5841=CIRCLE ( 'NONE', #30342, 18.00000000000000000 ) ;
#5886=ORIENTED_EDGE ( 'NONE', *, *, #27285, .T. ) ;
#5902=CARTESIAN_POINT ( 'NONE',  ( -27.50000000000001066, 1.342284157770889275, -18.00000000000000355 ) ) ;
#5970=ADVANCED_FACE ( 'NONE', ( #16403 ), #26030, .T. ) ;
#6035=ORIENTED_EDGE ( 'NONE', *, *, #28476, .T. ) ;
#6040=DIRECTION ( 'NONE',  ( 0.000000000000000000, 0.000000000000000000, 1.000000000000000000 ) ) ;
#6145=FACE_OUTER_BOUND ( 'NONE', #2468, .T. ) ;
#6166=EDGE_CURVE ( 'NONE', #26131, #24999, #20581, .T. ) ;
#6180=EDGE_LOOP ( 'NONE', ( #24709, #24755, #27302 ) ) ;
#6213=CARTESIAN_POINT ( 'NONE',  ( 27.50000000000001066, -15.87713240271473580, -15.54379906938135214 ) ) ;
#6353=AXIS2_PLACEMENT_3D ( 'NONE', #18148, #7081, #25470 ) ;
#6373=CARTESIAN_POINT ( 'NONE',  ( -12.58016597185465280, 24.49110259512896448, -0.01440555954223410491 ) ) ;
#6378=DIRECTION ( 'NONE',  ( 0.000000000000000000, 0.000000000000000000, 1.000000000000000000 ) ) ;
#6468=FACE_BOUND ( 'NONE', #6887, .T. ) ;
#6496=CARTESIAN_POINT ( 'NONE',  ( -13.75000000000001954, 23.81569860407205752, 0.000000000000000000 ) ) ;
#6497=CIRCLE ( 'NONE', #7062, 27.50000000000000355 ) ;
#6565=EDGE_CURVE ( 'NONE', #11757, #8265, #15081, .T. ) ;
#6602=EDGE_CURVE ( 'NONE', #23832, #31055, #10813, .T. ) ;
#6673=EDGE_CURVE ( 'NONE', #22495, #355, #9133, .T. ) ;
#6719=CARTESIAN_POINT ( 'NONE',  ( -9.092171885314261459, 26.50489691992488162, -0.2827231011780766967 ) ) ;
#6751=CARTESIAN_POINT ( 'NONE',  ( 27.50000000000000355, 0.000000000000000000, -18.00000000000000000 ) ) ;
#6767=FILL_AREA_STYLE ('',( #24659 ) ) ;
#6771=ORIENTED_EDGE ( 'NONE', *, *, #27793, .T. ) ;
#6816=ORIENTED_EDGE ( 'NONE', *, *, #5748, .F. ) ;
#6887=EDGE_LOOP ( 'NONE', ( #8449, #31579 ) ) ;
#6898=VERTEX_POINT ( 'NONE', #17991 ) ;
#6947=DIRECTION ( 'NONE',  ( -0.000000000000000000, -0.000000000000000000, 1.000000000000000000 ) ) ;
#7025=CARTESIAN_POINT ( 'NONE',  ( -16.00000000000000000, 1.959434878635765131E-15, -16.57418492358057094 ) ) ;
#7032=ORIENTED_EDGE ( 'NONE', *, *, #31439, .T. ) ;
#7062=AXIS2_PLACEMENT_3D ( 'NONE', #26285, #2959, #23896 ) ;
#7081=DIRECTION ( 'NONE',  ( -0.000000000000000000, -0.000000000000000000, 1.000000000000000000 ) ) ;
#7117=CARTESIAN_POINT ( 'NONE',  ( 0.000000000000000000, 0.000000000000000000, -17.97459999999999525 ) ) ;
#7163=ORIENTED_EDGE ( 'NONE', *, *, #27591, .T. ) ;
#7187=ORIENTED_EDGE ( 'NONE', *, *, #31448, .T. ) ;
#7249=DIRECTION ( 'NONE',  ( -0.000000000000000000, -0.000000000000000000, 1.000000000000000000 ) ) ;
#7275=CARTESIAN_POINT ( 'NONE',  ( 0.000000000000000000, 0.000000000000000000, -18.00000000000000000 ) ) ;
#7295=CIRCLE ( 'NONE', #25799, 18.00000000000000000 ) ;
#7334=VERTEX_POINT ( 'NONE', #5699 ) ;
#7355=CARTESIAN_POINT ( 'NONE',  ( -4.515071337844649868, -29.14748715311448279, -1.088725517910814400 ) ) ;
#7387=CARTESIAN_POINT ( 'NONE',  ( -27.50000000000000000, -15.87713240271474824, -2.456200930618646971 ) ) ;
#7403=ORIENTED_EDGE ( 'NONE', *, *, #19488, .F. ) ;
#7447=CARTESIAN_POINT ( 'NONE',  ( 0.000000000000000000, 0.000000000000000000, -17.97459999999999525 ) ) ;
#7456=CONICAL_SURFACE ( 'NONE', #26477, 15.79999999999999538, 0.9599310885968802554 ) ;
#7473=EDGE_CURVE ( 'NONE', #21688, #22734, #17075, .T. ) ;
#7505=VERTEX_POINT ( 'NONE', #22729 ) ;
#7525=DIRECTION ( 'NONE',  ( 1.000000000000000000, 0.000000000000000000, 0.000000000000000000 ) ) ;
#7570=CARTESIAN_POINT ( 'NONE',  ( -27.50000000000000000, 2.688867821578062145, -0.05704280876259919253 ) ) ;
#7627=ORIENTED_EDGE ( 'NONE', *, *, #10604, .T. ) ;
#7732=CARTESIAN_POINT ( 'NONE',  ( -27.50000000000000000, 6.731471899275967452, -0.4522261538067093301 ) ) ;
#7751=FACE_OUTER_BOUND ( 'NONE', #1183, .T. ) ;
#7756=DIRECTION ( 'NONE',  ( -0.000000000000000000, -0.000000000000000000, 1.000000000000000000 ) ) ;
#7758=DIRECTION ( 'NONE',  ( -1.000000000000000000, 0.000000000000000000, 0.000000000000000000 ) ) ;
#7834=ORIENTED_EDGE ( 'NONE', *, *, #31181, .T. ) ;
#7878=EDGE_CURVE ( 'NONE', #8582, #28277, #23384, .T. ) ;
#7900=CARTESIAN_POINT ( 'NONE',  ( 16.66875746037182537, 22.13055319862716175, -0.1142222407377223303 ) ) ;
#7946=EDGE_CURVE ( 'NONE', #18759, #1785, #6497, .T. ) ;
#7966=UNCERTAINTY_MEASURE_WITH_UNIT (LENGTH_MEASURE( 1.000000000000000082E-05 ), #24310, 'distance_accuracy_value', 'NONE');
#7974=SURFACE_SIDE_STYLE ('',( #16117 ) ) ;
#8013=DIRECTION ( 'NONE',  ( -0.000000000000000000, -0.000000000000000000, 1.000000000000000000 ) ) ;
#8033=CARTESIAN_POINT ( 'NONE',  ( -13.75000000000001954, 23.81569860407205752, -18.00000000000000000 ) ) ;
#8047=CARTESIAN_POINT ( 'NONE',  ( -4.336808689942017736E-14, -31.75426480542944319, -15.54379906938135214 ) ) ;
#8074=ORIENTED_EDGE ( 'NONE', *, *, #28746, .T. ) ;
#8081=ORIENTED_EDGE ( 'NONE', *, *, #28510, .F. ) ;
#8095=CARTESIAN_POINT ( 'NONE',  ( 0.000000000000000000, 0.000000000000000000, -18.00000000000000000 ) ) ;
#8129=ORIENTED_EDGE ( 'NONE', *, *, #4121, .F. ) ;
#8134=CARTESIAN_POINT ( 'NONE',  ( -16.00000000000000000, 1.959434878635765131E-15, -1.400415076419418092 ) ) ;
#8226=CARTESIAN_POINT ( 'NONE',  ( -27.50000000000000000, -2.682974265912531742, 2.093865445612630438E-15 ) ) ;
#8251=DIRECTION ( 'NONE',  ( -0.000000000000000000, -0.000000000000000000, 1.000000000000000000 ) ) ;
#8257=AXIS2_PLACEMENT_3D ( 'NONE', #19279, #32895, #4103 ) ;
#8265=VERTEX_POINT ( 'NONE', #12123 ) ;
#8271=DIRECTION ( 'NONE',  ( -0.000000000000000000, -0.000000000000000000, 1.000000000000000000 ) ) ;
#8307=DIRECTION ( 'NONE',  ( -0.000000000000000000, 0.000000000000000000, -1.000000000000000000 ) ) ;
#8449=ORIENTED_EDGE ( 'NONE', *, *, #33554, .F. ) ;
#8453=ORIENTED_EDGE ( 'NONE', *, *, #2694, .F. ) ;
#8577=CARTESIAN_POINT ( 'NONE',  ( -27.50000000000000000, 15.87713240271469672, -18.00000000000000000 ) ) ;
#8582=VERTEX_POINT ( 'NONE', #26737 ) ;
#8640=EDGE_CURVE ( 'NONE', #26498, #29684, #20855, .T. ) ;
#8655=VERTEX_POINT ( 'NONE', #24696 ) ;
#8683=CARTESIAN_POINT ( 'NONE',  ( -13.75000000000001243, -23.81569860407206107, -18.00000000000000000 ) ) ;
#8700=ORIENTED_EDGE ( 'NONE', *, *, #20818, .T. ) ;
#8719=CARTESIAN_POINT ( 'NONE',  ( -27.50000000000000000, -15.87713240271474824, -15.54379906938135214 ) ) ;
#8731=CARTESIAN_POINT ( 'NONE',  ( 0.000000000000000000, 0.000000000000000000, -18.00000000000000000 ) ) ;
#8741=FACE_OUTER_BOUND ( 'NONE', #1415, .T. ) ;
#8744=EDGE_CURVE ( 'NONE', #29684, #6898, #19641, .T. ) ;
#8780=ORIENTED_EDGE ( 'NONE', *, *, #9157, .T. ) ;
#8795=DIRECTION ( 'NONE',  ( -1.000000000000000000, 0.000000000000000000, 0.000000000000000000 ) ) ;
#8818=ADVANCED_FACE ( 'NONE', ( #6468, #16851 ), #32859, .F. ) ;
#8825=DIRECTION ( 'NONE',  ( 0.000000000000000000, 0.000000000000000000, 1.000000000000000000 ) ) ;
#8848=ORIENTED_EDGE ( 'NONE', *, *, #8744, .T. ) ;
#8866=CIRCLE ( 'NONE', #24117, 27.50000000000000355 ) ;
#8872=CARTESIAN_POINT ( 'NONE',  ( 0.000000000000000000, 0.000000000000000000, 0.000000000000000000 ) ) ;
#8907=ORIENTED_EDGE ( 'NONE', *, *, #31439, .F. ) ;
#8923=LINE ( 'NONE', #1425, #33260 ) ;
#8925=CARTESIAN_POINT ( 'NONE',  ( 16.00000000000000000, 0.000000000000000000, -18.00000000000000000 ) ) ;
#8931=EDGE_LOOP ( 'NONE', ( #31343, #8848, #29305 ) ) ;
#8950=DIRECTION ( 'NONE',  ( 0.5000000000000008882, 0.8660254037844382635, -0.000000000000000000 ) ) ;
#9071=CARTESIAN_POINT ( 'NONE',  ( -16.08713178458081572, -22.46635493911272619, -17.92845254598169547 ) ) ;
#9096=CARTESIAN_POINT ( 'NONE',  ( -13.16654248868335841, 24.15255795529145288, 2.021585300780266894E-15 ) ) ;
#9102=VECTOR ( 'NONE', #3639, 1000.000000000000000 ) ;
#9111=EDGE_CURVE ( 'NONE', #12301, #12567, #31769, .T. ) ;
#9116=CONICAL_SURFACE ( 'NONE', #21639, 27.50000000000000355, 1.047197551196595411 ) ;
#9133=LINE ( 'NONE', #27524, #15152 ) ;
#9142=AXIS2_PLACEMENT_3D ( 'NONE', #27179, #14226, #32115 ) ;
#9149=PRESENTATION_STYLE_ASSIGNMENT (( #26873 ) ) ;
#9157=EDGE_CURVE ( 'NONE', #7334, #7505, #31945, .T. ) ;
#9205=EDGE_LOOP ( 'NONE', ( #19411, #7032, #13803 ) ) ;
#9211=CARTESIAN_POINT ( 'NONE',  ( 0.000000000000000000, 0.000000000000000000, 0.000000000000000000 ) ) ;
#9217=CARTESIAN_POINT ( 'NONE',  ( -18.40606158072672827, 21.12752019707600581, -0.2340887491524386022 ) ) ;
#9261=DIRECTION ( 'NONE',  ( 1.000000000000000000, 0.000000000000000000, 0.000000000000000000 ) ) ;
#9267=ORIENTED_EDGE ( 'NONE', *, *, #17655, .T. ) ;
#9290=CARTESIAN_POINT ( 'NONE',  ( 27.50000000000001066, -15.87713240271473580, -15.54379906938135214 ) ) ;
#9427=CARTESIAN_POINT ( 'NONE',  ( 0.000000000000000000, 0.000000000000000000, -18.00000000000000000 ) ) ;
#9531=ORIENTED_EDGE ( 'NONE', *, *, #19129, .T. ) ;
#9538=DIRECTION ( 'NONE',  ( 0.000000000000000000, 0.000000000000000000, -1.000000000000000000 ) ) ;
#9554=CARTESIAN_POINT ( 'NONE',  ( -11.40740920524442004, -25.16819403002536859, -1.393199791643873198E-14 ) ) ;
#9582=ORIENTED_EDGE ( 'NONE', *, *, #15203, .F. ) ;
#9590=CARTESIAN_POINT ( 'NONE',  ( -14.33345751131668777, -23.47883925285269413, -1.404041813368736288E-14 ) ) ;
#9614=CARTESIAN_POINT ( 'NONE',  ( -27.50000000000000000, -15.87713240271473225, -18.00000000000000000 ) ) ;
#9706=ORIENTED_EDGE ( 'NONE', *, *, #4528, .F. ) ;
#9737=EDGE_CURVE ( 'NONE', #25250, #355, #15611, .T. ) ;
#9847=DIRECTION ( 'NONE',  ( -1.000000000000000000, 0.000000000000000000, 0.000000000000000000 ) ) ;
#9904=CARTESIAN_POINT ( 'NONE',  ( -13.75000000000001243, -23.81569860407206107, 0.000000000000000000 ) ) ;
#9947=CARTESIAN_POINT ( 'NONE',  ( 27.50000000000000355, -15.87713240271473580, -18.00000000000000000 ) ) ;
#10016=ORIENTED_EDGE ( 'NONE', *, *, #21184, .F. ) ;
#10019=ORIENTED_EDGE ( 'NONE', *, *, #9111, .F. ) ;
#10026=ADVANCED_FACE ( 'NONE', ( #18060, #5114 ), #15668, .T. ) ;
#10030=FACE_OUTER_BOUND ( 'NONE', #4888, .T. ) ;
#10123=CARTESIAN_POINT ( 'NONE',  ( 27.50000000000000711, 5.390523180938862957, -0.2837416352459796176 ) ) ;
#10176=CARTESIAN_POINT ( 'NONE',  ( 27.50000000000000355, 15.87713240271474291, -15.54379906938135214 ) ) ;
#10196=CARTESIAN_POINT ( 'NONE',  ( 16.66875746037182537, 22.13055319862716175, -17.88577775926227531 ) ) ;
#10198=DIRECTION ( 'NONE',  ( 0.8191520442889912434, 0.000000000000000000, 0.5735764363510469366 ) ) ;
#10257=CARTESIAN_POINT ( 'NONE',  ( -16.09259079475562615, 22.46320317811876421, -18.00000000000000711 ) ) ;
#10324=DIRECTION ( 'NONE',  ( 1.000000000000000000, 0.000000000000000000, 0.000000000000000000 ) ) ;
#10406=DIRECTION ( 'NONE',  ( -1.000000000000000000, 0.000000000000000000, 0.000000000000000000 ) ) ;
#10477=CARTESIAN_POINT ( 'NONE',  ( 13.75000000000000888, -23.81569860407206463, 0.000000000000000000 ) ) ;
#10479=ORIENTED_EDGE ( 'NONE', *, *, #13743, .F. ) ;
#10482=ORIENTED_EDGE ( 'NONE', *, *, #28130, .T. ) ;
#10498=CARTESIAN_POINT ( 'NONE',  ( 27.50000000000000355, 0.000000000000000000, 0.000000000000000000 ) ) ;
#10533=CARTESIAN_POINT ( 'NONE',  ( 18.40782811468575986, 21.12650028821923698, -17.71727689882192891 ) ) ;
#10550=ADVANCED_FACE ( 'NONE', ( #10030 ), #9116, .T. ) ;
#10604=EDGE_CURVE ( 'NONE', #6898, #23864, #17158, .T. ) ;
#10625=CARTESIAN_POINT ( 'NONE',  ( 22.99387487948480668, 18.47874495404628092, -1.090893241169154315 ) ) ;
#10648=ADVANCED_FACE ( 'NONE', ( #28413 ), #4903, .F. ) ;
#10693=( NAMED_UNIT ( * ) SI_UNIT ( $, .STERADIAN. ) SOLID_ANGLE_UNIT ( ) );
#10802=EDGE_LOOP ( 'NONE', ( #10830, #2122, #11554, #493 ) ) ;
#10813=CIRCLE ( 'NONE', #1556, 27.50000000000000355 ) ;
#10814=AXIS2_PLACEMENT_3D ( 'NONE', #7117, #31131, #4897 ) ;
#10830=ORIENTED_EDGE ( 'NONE', *, *, #395, .F. ) ;
#10925=EDGE_CURVE ( 'NONE', #22734, #31784, #32179, .T. ) ;
#11005=ADVANCED_FACE ( 'NONE', ( #19985 ), #1258, .T. ) ;
#11011=B_SPLINE_CURVE_WITH_KNOTS ( 'NONE', 3,
 ( #33578, #2578, #15845, #26234, #10257, #28469 ),
 .UNSPECIFIED., .F., .F.,
 ( 4, 2, 4 ),
 ( 2.380727409112127398E-07, 0.008032766472079759176, 0.01606529487141860474 ),
 .UNSPECIFIED. ) ;
#11023=SHAPE_REPRESENTATION_RELATIONSHIP ( 'NONE' , 'NONE' ,  #16299, #13278 ) ;
#11054=EDGE_CURVE ( 'NONE', #18759, #12567, #28775, .T. ) ;
#11080=DIRECTION ( 'NONE',  ( 0.000000000000000000, 0.000000000000000000, -1.000000000000000000 ) ) ;
#11271=CONICAL_SURFACE ( 'NONE', #33574, 27.50000000000000355, 1.047197551196595411 ) ;
#11292=DIRECTION ( 'NONE',  ( 1.000000000000000000, 0.000000000000000000, 0.000000000000000000 ) ) ;
#11433=CARTESIAN_POINT ( 'NONE',  ( -27.50000000000000000, 15.87713240271469672, -2.456200930618631428 ) ) ;
#11440=CARTESIAN_POINT ( 'NONE',  ( -22.98492866215539010, 18.48391005502964646, -1.088725517910800189 ) ) ;
#11469=CARTESIAN_POINT ( 'NONE',  ( -16.66875746037182537, -22.13055319862718662, -17.88577775926225755 ) ) ;
#11554=ORIENTED_EDGE ( 'NONE', *, *, #29970, .T. ) ;
#11597=AXIS2_PLACEMENT_3D ( 'NONE', #33182, #6947, #4212 ) ;
#11750=EDGE_LOOP ( 'NONE', ( #6035, #32497, #2425, #10019, #16643, #33461 ) ) ;
#11757=VERTEX_POINT ( 'NONE', #30003 ) ;
#11765=PLANE ( 'NONE',  #22796 ) ;
#11777=CARTESIAN_POINT ( 'NONE',  ( 13.75000000000000888, -23.81569860407206463, 0.000000000000000000 ) ) ;
#11834=ORIENTED_EDGE ( 'NONE', *, *, #8744, .F. ) ;
#11873=CONICAL_SURFACE ( 'NONE', #10814, 18.00000000000000711, 0.9599310885968802554 ) ;
#11920=ORIENTED_EDGE ( 'NONE', *, *, #10925, .F. ) ;
#11941=DIRECTION ( 'NONE',  ( 0.000000000000000000, 0.000000000000000000, 1.000000000000000000 ) ) ;
#11943=AXIS2_PLACEMENT_3D ( 'NONE', #21674, #21171, #16383 ) ;
#11997=ADVANCED_FACE ( 'NONE', ( #24174 ), #22517, .T. ) ;
#12044=AXIS2_PLACEMENT_3D ( 'NONE', #22206, #32595, #9261 ) ;
#12123=CARTESIAN_POINT ( 'NONE',  ( -27.50000000000000000, 15.87713240271474824, -15.54379906938135214 ) ) ;
#12132=VECTOR ( 'NONE', #2152, 1000.000000000000000 ) ;
#12175=CARTESIAN_POINT ( 'NONE',  ( -27.50000000000001066, -2.682974265912532186, -18.00000000000001066 ) ) ;
#12199=DIRECTION ( 'NONE',  ( 0.000000000000000000, 0.000000000000000000, -1.000000000000000000 ) ) ;
#12230=DIRECTION ( 'NONE',  ( -0.000000000000000000, 0.000000000000000000, -1.000000000000000000 ) ) ;
#12301=VERTEX_POINT ( 'NONE', #8719 ) ;
#12342=CARTESIAN_POINT ( 'NONE',  ( -27.50000000000001066, -14.58598892539969860, -15.91652008647649197 ) ) ;
#12399=CARTESIAN_POINT ( 'NONE',  ( 16.08713178458081217, 22.46635493911270132, -17.92845254598171678 ) ) ;
#12423=EDGE_LOOP ( 'NONE', ( #7627, #10479, #16911 ) ) ;
#12433=EDGE_LOOP ( 'NONE', ( #20263, #27660, #30330 ) ) ;
#12457=DIRECTION ( 'NONE',  ( 0.000000000000000000, 0.000000000000000000, 1.000000000000000000 ) ) ;
#12477=B_SPLINE_CURVE_WITH_KNOTS ( 'NONE', 3,
 ( #22673, #27954, #7355, #1553, #9554, #9904 ),
 .UNSPECIFIED., .F., .F.,
 ( 4, 2, 4 ),
 ( 2.380727409348927899E-07, 0.008032766472079795605, 0.01606529487141865678 ),
 .UNSPECIFIED. ) ;
#12482=EDGE_CURVE ( 'NONE', #33588, #18759, #12477, .T. ) ;
#12563=AXIS2_PLACEMENT_3D ( 'NONE', #28623, #8013, #18399 ) ;
#12567=VERTEX_POINT ( 'NONE', #5457 ) ;
#12702=ADVANCED_FACE ( 'NONE', ( #20461 ), #15680, .F. ) ;
#12706=CARTESIAN_POINT ( 'NONE',  ( 27.50000000000000355, 15.87713240271474291, -15.54379906938135214 ) ) ;
#12941=EDGE_LOOP ( 'NONE', ( #22343, #817, #13471, #28985 ) ) ;
#12951=ORIENTED_EDGE ( 'NONE', *, *, #3972, .F. ) ;
#12953=CONICAL_SURFACE ( 'NONE', #24910, 27.50000000000000355, 1.047197551196595411 ) ;
#12968=B_SPLINE_CURVE_WITH_KNOTS ( 'NONE', 3,
 ( #16052, #13496, #7570, #33621, #7732, #18118, #2621, #5166 ),
 .UNSPECIFIED., .F., .F.,
 ( 4, 2, 2, 4 ),
 ( 0.04438889715320012280, 0.04840678451617880934, 0.05242467187915750282, 0.06046044660511487590 ),
 .UNSPECIFIED. ) ;
#12988=CARTESIAN_POINT ( 'NONE',  ( 9.092171885314263236, -26.50489691992491359, -17.71727689882190404 ) ) ;
#13043=CARTESIAN_POINT ( 'NONE',  ( 27.50000000000000711, -5.348566131067986618, -0.2306174136865334345 ) ) ;
#13060=ORIENTED_EDGE ( 'NONE', *, *, #6602, .F. ) ;
#13188=ORIENTED_EDGE ( 'NONE', *, *, #2334, .F. ) ;
#13278=ADVANCED_BREP_SHAPE_REPRESENTATION ( '', ( #23813, #2404 ), #29629 ) ;
#13442=DIRECTION ( 'NONE',  ( 0.000000000000000000, 0.000000000000000000, -1.000000000000000000 ) ) ;
#13471=ORIENTED_EDGE ( 'NONE', *, *, #27442, .T. ) ;
#13472=CIRCLE ( 'NONE', #9142, 27.50000000000000355 ) ;
#13496=CARTESIAN_POINT ( 'NONE',  ( -27.49999999999999289, 1.342284157770882835, 1.943940613948618489E-15 ) ) ;
#13543=EDGE_CURVE ( 'NONE', #26498, #11757, #30571, .T. ) ;
#13634=ORIENTED_EDGE ( 'NONE', *, *, #6673, .T. ) ;
#13658=CARTESIAN_POINT ( 'NONE',  ( 27.50000000000000711, -9.324699302609174012, -17.12819780694305649 ) ) ;
#13682=ADVANCED_FACE ( 'NONE', ( #32804 ), #32743, .T. ) ;
#13700=DIRECTION ( 'NONE',  ( 0.000000000000000000, -0.000000000000000000, 1.000000000000000000 ) ) ;
#13727=CARTESIAN_POINT ( 'NONE',  ( 9.093938419273294826, 26.50387701106810923, -0.2340887491524412944 ) ) ;
#13743=EDGE_CURVE ( 'NONE', #28277, #23864, #19343, .T. ) ;
#13794=CARTESIAN_POINT ( 'NONE',  ( -9.092171885314263236, 26.50489691992488517, -17.71727689882192536 ) ) ;
#13803=ORIENTED_EDGE ( 'NONE', *, *, #1901, .F. ) ;
#13853=EDGE_LOOP ( 'NONE', ( #30110, #32539, #8700, #15532 ) ) ;
#13889=FACE_OUTER_BOUND ( 'NONE', #2213, .T. ) ;
#13891=EDGE_LOOP ( 'NONE', ( #27720, #12951, #14194 ) ) ;
#13986=VECTOR ( 'NONE', #14653, 1000.000000000000000 ) ;
#14036=AXIS2_PLACEMENT_3D ( 'NONE', #24345, #11080, #3064 ) ;
#14077=CARTESIAN_POINT ( 'NONE',  ( -27.50000000000001066, 13.30988860919481809, -16.28489851701342417 ) ) ;
#14155=CARTESIAN_POINT ( 'NONE',  ( 27.50000000000000355, 15.87713240271469317, -18.00000000000000000 ) ) ;
#14191=DIRECTION ( 'NONE',  ( 1.000000000000000000, 0.000000000000000000, 0.000000000000000000 ) ) ;
#14194=ORIENTED_EDGE ( 'NONE', *, *, #11054, .F. ) ;
#14204=DIRECTION ( 'NONE',  ( 1.000000000000000000, 0.000000000000000000, 0.000000000000000000 ) ) ;
#14226=DIRECTION ( 'NONE',  ( -0.000000000000000000, 0.000000000000000000, -1.000000000000000000 ) ) ;
#14259=ORIENTED_EDGE ( 'NONE', *, *, #28476, .F. ) ;
#14360=DIRECTION ( 'NONE',  ( 0.000000000000000000, 0.000000000000000000, 1.000000000000000000 ) ) ;
#14366=DIRECTION ( 'NONE',  ( 1.000000000000000000, 0.000000000000000000, 0.000000000000000000 ) ) ;
#14416=CARTESIAN_POINT ( 'NONE',  ( 0.000000000000000000, 0.000000000000000000, -18.00000000000000000 ) ) ;
#14490=AXIS2_PLACEMENT_3D ( 'NONE', #8731, #33673, #11292 ) ;
#14505=ORIENTED_EDGE ( 'NONE', *, *, #31181, .F. ) ;
#14532=CARTESIAN_POINT ( 'NONE',  ( -18.40782811468575986, -21.12650028821925829, -0.2827231011780881320 ) ) ;
#14535=CARTESIAN_POINT ( 'NONE',  ( -27.50000000000000000, -15.87713240271474824, -2.456200930618646971 ) ) ;
#14546=CARTESIAN_POINT ( 'NONE',  ( 6.938893903907228378E-15, 31.75426480542944319, -2.456200930618646971 ) ) ;
#14556=CARTESIAN_POINT ( 'NONE',  ( -27.50000000000000000, -15.87713240271474824, -15.54379906938135214 ) ) ;
#14587=AXIS2_PLACEMENT_3D ( 'NONE', #8095, #8251, #5518 ) ;
#14645=EDGE_LOOP ( 'NONE', ( #2698, #25469, #24037, #14505, #26092, #4858 ) ) ;
#14653=DIRECTION ( 'NONE',  ( -0.000000000000000000, -0.000000000000000000, 1.000000000000000000 ) ) ;
#14680=FACE_OUTER_BOUND ( 'NONE', #14645, .T. ) ;
#14729=CARTESIAN_POINT ( 'NONE',  ( -2.249320974685042440, -30.45561873520117757, -16.29357272760981701 ) ) ;
#14825=AXIS2_PLACEMENT_3D ( 'NONE', #32440, #6040, #16431 ) ;
#14835=CARTESIAN_POINT ( 'NONE',  ( 7.331804101520335523E-16, -31.75426480542945740, -18.00000000000000000 ) ) ;
#14996=CARTESIAN_POINT ( 'NONE',  ( 0.000000000000000000, 0.000000000000000000, -17.97459999999999525 ) ) ;
#15041=DIRECTION ( 'NONE',  ( -0.000000000000000000, -0.000000000000000000, 1.000000000000000000 ) ) ;
#15081=B_SPLINE_CURVE_WITH_KNOTS ( 'NONE', 3,
 ( #27024, #5902, #24642, #26687, #16126, #3348, #14077, #31963 ),
 .UNSPECIFIED., .F., .F.,
 ( 4, 2, 2, 4 ),
 ( 0.04438889715320012280, 0.04840678451617882322, 0.05242467187915753057, 0.06046044660511493141 ),
 .UNSPECIFIED. ) ;
#15149=ORIENTED_EDGE ( 'NONE', *, *, #4528, .T. ) ;
#15152=VECTOR ( 'NONE', #24808, 1000.000000000000000 ) ;
#15164=CONICAL_SURFACE ( 'NONE', #18457, 27.50000000000000355, 1.047197551196595411 ) ;
#15203=EDGE_CURVE ( 'NONE', #8265, #253, #25136, .T. ) ;
#15215=CARTESIAN_POINT ( 'NONE',  ( -13.75000000000001243, -23.81569860407206107, 0.000000000000000000 ) ) ;
#15274=( NAMED_UNIT ( * ) SI_UNIT ( $, .STERADIAN. ) SOLID_ANGLE_UNIT ( ) );
#15289=CARTESIAN_POINT ( 'NONE',  ( 0.000000000000000000, 0.000000000000000000, -18.00000000000000000 ) ) ;
#15290=CARTESIAN_POINT ( 'NONE',  ( -15.79999999999999538, 1.934941942652817234E-15, -1.540456584061364431 ) ) ;
#15329=ORIENTED_EDGE ( 'NONE', *, *, #6602, .T. ) ;
#15368=CARTESIAN_POINT ( 'NONE',  ( 12.58016597185466168, -24.49110259512899290, -17.98559444045774569 ) ) ;
#15387=CARTESIAN_POINT ( 'NONE',  ( 14.33345751131668599, 23.47883925285266926, 5.014435047745465896E-16 ) ) ;
#15505=CARTESIAN_POINT ( 'NONE',  ( -6.938893903907228378E-15, 31.75426480542944319, -18.00000000000000000 ) ) ;
#15532=ORIENTED_EDGE ( 'NONE', *, *, #29970, .F. ) ;
#15551=CARTESIAN_POINT ( 'NONE',  ( 19.55945325266599966, 20.46160920480079781, -0.4491195576436673997 ) ) ;
#15585=CARTESIAN_POINT ( 'NONE',  ( 27.49999999999999645, -10.64700562007353923, -1.134120025693882594 ) ) ;
#15611=CIRCLE ( 'NONE', #32478, 18.00000000000000711 ) ;
#15617=FACE_OUTER_BOUND ( 'NONE', #12423, .T. ) ;
#15638=FACE_OUTER_BOUND ( 'NONE', #10802, .T. ) ;
#15639=AXIS2_PLACEMENT_3D ( 'NONE', #15505, #26071, #10406 ) ;
#15668=PLANE ( 'NONE',  #15639 ) ;
#15680=CYLINDRICAL_SURFACE ( 'NONE', #29056, 18.00000000000000355 ) ;
#15681=DIRECTION ( 'NONE',  ( -1.000000000000000000, 0.000000000000000000, 0.000000000000000000 ) ) ;
#15778=EDGE_LOOP ( 'NONE', ( #5886, #15329, #8081 ) ) ;
#15785=B_SPLINE_CURVE_WITH_KNOTS ( 'NONE', 3,
 ( #19949, #28126, #30348, #4787, #24735, #11777 ),
 .UNSPECIFIED., .F., .F.,
 ( 4, 2, 4 ),
 ( 2.380727408751203747E-07, 0.008032766472079738360, 0.01606529487141860127 ),
 .UNSPECIFIED. ) ;
#15817=AXIS2_PLACEMENT_3D ( 'NONE', #21124, #23014, #15681 ) ;
#15845=CARTESIAN_POINT ( 'NONE',  ( -22.98492866215537589, 18.48391005502966777, -16.91127448208919759 ) ) ;
#15913=DIRECTION ( 'NONE',  ( 1.000000000000000000, 0.000000000000000000, 0.000000000000000000 ) ) ;
#15988=ORIENTED_EDGE ( 'NONE', *, *, #28019, .T. ) ;
#16033=CARTESIAN_POINT ( 'NONE',  ( 13.75000000000000888, -23.81569860407206463, -18.00000000000000000 ) ) ;
#16052=CARTESIAN_POINT ( 'NONE',  ( -27.50000000000000355, 0.000000000000000000, 0.000000000000000000 ) ) ;
#16072=ORIENTED_EDGE ( 'NONE', *, *, #9737, .F. ) ;
#16117=SURFACE_STYLE_FILL_AREA ( #21563 ) ;
#16126=CARTESIAN_POINT ( 'NONE',  ( -27.50000000000000711, 6.731471899275991433, -17.54777384619328373 ) ) ;
#16176=VECTOR ( 'NONE', #4321, 1000.000000000000000 ) ;
#16197=CARTESIAN_POINT ( 'NONE',  ( -18.00000000000000711, 0.000000000000000000, -17.97459999999999525 ) ) ;
#16216=CARTESIAN_POINT ( 'NONE',  ( 27.50000000000000711, -5.348566131067995499, -17.76938258631346912 ) ) ;
#16256=CARTESIAN_POINT ( 'NONE',  ( 0.000000000000000000, 0.000000000000000000, 3.469446951953614189E-15 ) ) ;
#16289=CARTESIAN_POINT ( 'NONE',  ( 6.938893903907228378E-15, 31.75426480542944319, -2.456200930618646971 ) ) ;
#16299=SHAPE_REPRESENTATION ( 'hex thin nut chamfered gradeab_iso_ISO - 4035 - M36 - N', ( #2404 ), #29629 ) ;
#16303=B_SPLINE_CURVE_WITH_KNOTS ( 'NONE', 3,
 ( #20678, #27998, #17957, #10123, #20837, #2454, #17435, #25612 ),
 .UNSPECIFIED., .F., .F.,
 ( 4, 2, 2, 4 ),
 ( 0.04438889715320012974, 0.04840678451617883016, 0.05242467187915753057, 0.06046044660511493835 ),
 .UNSPECIFIED. ) ;
#16359=ADVANCED_FACE ( 'NONE', ( #14680 ), #24906, .T. ) ;
#16383=DIRECTION ( 'NONE',  ( -1.000000000000000000, 1.776356839400250465E-15, 0.000000000000000000 ) ) ;
#16388=FACE_OUTER_BOUND ( 'NONE', #3049, .T. ) ;
#16403=FACE_OUTER_BOUND ( 'NONE', #12433, .T. ) ;
#16431=DIRECTION ( 'NONE',  ( 1.000000000000000000, 0.000000000000000000, 0.000000000000000000 ) ) ;
#16643=ORIENTED_EDGE ( 'NONE', *, *, #19129, .F. ) ;
#16718=CARTESIAN_POINT ( 'NONE',  ( 27.50000000000000355, -14.58598892539968972, -15.91652008647648842 ) ) ;
#16722=ORIENTED_EDGE ( 'NONE', *, *, #31660, .F. ) ;
#16783=VERTEX_POINT ( 'NONE', #26416 ) ;
#16802=CARTESIAN_POINT ( 'NONE',  ( 1.734723475976807094E-14, 31.75426480542944319, -15.54379906938135214 ) ) ;
#16805=VECTOR ( 'NONE', #1395, 1000.000000000000000 ) ;
#16851=FACE_OUTER_BOUND ( 'NONE', #28284, .T. ) ;
#16861=ORIENTED_EDGE ( 'NONE', *, *, #4127, .F. ) ;
#16885=CARTESIAN_POINT ( 'NONE',  ( 27.50000000000000355, -13.28298644054430255, -16.25870334244831383 ) ) ;
#16911=ORIENTED_EDGE ( 'NONE', *, *, #5748, .T. ) ;
#16945=PLANE ( 'NONE',  #24337 ) ;
#16958=AXIS2_PLACEMENT_3D ( 'NONE', #14416, #17474, #3852 ) ;
#17029=AXIS2_PLACEMENT_3D ( 'NONE', #25031, #1178, #30479 ) ;
#17075=B_SPLINE_CURVE_WITH_KNOTS ( 'NONE', 3,
 ( #32943, #9096, #6373, #3989, #20166, #6719, #27494, #22558, #4149, #14546 ),
 .UNSPECIFIED., .F., .F.,
 ( 4, 2, 2, 2, 4 ),
 ( 0.01606529487141860474, 0.01806591702017404724, 0.02006653916892948974, 0.02406778346644037475, 0.03207027206146213782 ),
 .UNSPECIFIED. ) ;
#17152=SURFACE_SIDE_STYLE ('',( #1322 ) ) ;
#17155=VERTEX_POINT ( 'NONE', #24618 ) ;
#17158=B_SPLINE_CURVE_WITH_KNOTS ( 'NONE', 3,
 ( #30803, #25684, #23466, #12399, #10196, #10533, #23301, #20913, #25514, #28068 ),
 .UNSPECIFIED., .F., .F.,
 ( 4, 2, 2, 2, 4 ),
 ( 0.01606529487141864984, 0.01806591702017408541, 0.02006653916892952097, 0.02406778346644038516, 0.03207027206146210313 ),
 .UNSPECIFIED. ) ;
#17287=ADVANCED_FACE ( 'NONE', ( #19003 ), #29393, .F. ) ;
#17302=CARTESIAN_POINT ( 'NONE',  ( 22.98492866215539365, -18.48391005502968198, -16.91127448208918338 ) ) ;
#17333=VERTEX_POINT ( 'NONE', #6213 ) ;
#17430=DIRECTION ( 'NONE',  ( 1.000000000000000000, 0.000000000000000000, 0.000000000000000000 ) ) ;
#17435=CARTESIAN_POINT ( 'NONE',  ( 27.50000000000000000, 13.30988860919481809, -1.715101482986582715 ) ) ;
#17457=ORIENTED_EDGE ( 'NONE', *, *, #10604, .F. ) ;
#17474=DIRECTION ( 'NONE',  ( 0.000000000000000000, -0.000000000000000000, 1.000000000000000000 ) ) ;
#17522=B_SPLINE_CURVE_WITH_KNOTS ( 'NONE', 3,
 ( #5164, #15387, #5328, #23722, #7900, #23399, #15551, #10625, #18281, #21162 ),
 .UNSPECIFIED., .F., .F.,
 ( 4, 2, 2, 2, 4 ),
 ( 0.01606529487141864984, 0.01806591702017408541, 0.02006653916892951403, 0.02406778346644038169, 0.03207027206146211007 ),
 .UNSPECIFIED. ) ;
#17543=ORIENTED_EDGE ( 'NONE', *, *, #26586, .T. ) ;
#17629=ORIENTED_EDGE ( 'NONE', *, *, #5018, .T. ) ;
#17630=CARTESIAN_POINT ( 'NONE',  ( -4.515071337844649868, -29.14748715311448279, -16.91127448208918338 ) ) ;
#17655=EDGE_CURVE ( 'NONE', #12301, #11757, #17848, .T. ) ;
#17666=STYLED_ITEM ( 'NONE', ( #29079 ), #13278 ) ;
#17789=CARTESIAN_POINT ( 'NONE',  ( 11.41286821541922336, -25.16504226903143859, -0.07154745401829853968 ) ) ;
#17848=B_SPLINE_CURVE_WITH_KNOTS ( 'NONE', 3,
 ( #14556, #12342, #1774, #27502, #4338, #20008, #12175, #30408 ),
 .UNSPECIFIED., .F., .F.,
 ( 4, 2, 2, 4 ),
 ( 0.02832689070575898985, 0.03234239231761927569, 0.03635789392947955806, 0.04438889715320012280 ),
 .UNSPECIFIED. ) ;
#17926=EDGE_CURVE ( 'NONE', #31055, #33588, #21947, .T. ) ;
#17957=CARTESIAN_POINT ( 'NONE',  ( 27.50000000000001066, 2.688867821578068806, -0.05704280876260246769 ) ) ;
#17969=CARTESIAN_POINT ( 'NONE',  ( 7.940546747334011890, -27.16978800334334920, -0.4491195576436878278 ) ) ;
#17991=CARTESIAN_POINT ( 'NONE',  ( 13.75000000000002487, 23.81569860407205397, -18.00000000000000000 ) ) ;
#17993=CARTESIAN_POINT ( 'NONE',  ( 27.50000000000000711, 10.70896984529284524, -16.90208611084169732 ) ) ;
#18002=DIRECTION ( 'NONE',  ( 0.000000000000000000, -0.000000000000000000, 1.000000000000000000 ) ) ;
#18060=FACE_BOUND ( 'NONE', #23854, .T. ) ;
#18118=CARTESIAN_POINT ( 'NONE',  ( -27.49999999999999645, 10.70896984529281859, -1.097913889158296019 ) ) ;
#18132=CARTESIAN_POINT ( 'NONE',  ( 12.58016597185466345, -24.49110259512898935, -0.01440555954224961507 ) ) ;
#18139=PLANE ( 'NONE',  #24679 ) ;
#18148=CARTESIAN_POINT ( 'NONE',  ( 0.000000000000000000, 0.000000000000000000, -16.57418492358057094 ) ) ;
#18159=CARTESIAN_POINT ( 'NONE',  ( 27.50000000000001776, -15.87713240271472870, -2.456200930618646971 ) ) ;
#18192=DIRECTION ( 'NONE',  ( -1.000000000000000000, 0.000000000000000000, 0.000000000000000000 ) ) ;
#18194=( LENGTH_UNIT ( ) NAMED_UNIT ( * ) SI_UNIT ( .MILLI., .METRE. ) );
#18253=ORIENTED_EDGE ( 'NONE', *, *, #6673, .F. ) ;
#18281=CARTESIAN_POINT ( 'NONE',  ( 25.25629716696159122, 17.17253483735094832, -1.708299986272424853 ) ) ;
#18308=VECTOR ( 'NONE', #25013, 1000.000000000000000 ) ;
#18399=DIRECTION ( 'NONE',  ( 1.000000000000000000, 0.000000000000000000, 0.000000000000000000 ) ) ;
#18417=CARTESIAN_POINT ( 'NONE',  ( -12.58016597185465457, 24.49110259512897159, -17.98559444045776345 ) ) ;
#18457=AXIS2_PLACEMENT_3D ( 'NONE', #22011, #8271, #2826 ) ;
#18563=ORIENTED_EDGE ( 'NONE', *, *, #24349, .T. ) ;
#18661=DIRECTION ( 'NONE',  ( -1.000000000000000000, 0.000000000000000000, 0.000000000000000000 ) ) ;
#18759=VERTEX_POINT ( 'NONE', #29024 ) ;
#18804=ORIENTED_EDGE ( 'NONE', *, *, #21851, .F. ) ;
#18926=ADVANCED_FACE ( 'NONE', ( #7751 ), #18139, .T. ) ;
#19003=FACE_OUTER_BOUND ( 'NONE', #12941, .T. ) ;
#19012=VERTEX_POINT ( 'NONE', #22188 ) ;
#19015=CARTESIAN_POINT ( 'NONE',  ( 27.50000000000001776, -15.87713240271472870, -2.456200930618646971 ) ) ;
#19019=CARTESIAN_POINT ( 'NONE',  ( 13.75000000000002487, 23.81569860407205397, 0.000000000000000000 ) ) ;
#19107=ADVANCED_FACE ( 'NONE', ( #8741 ), #22023, .T. ) ;
#19129=EDGE_CURVE ( 'NONE', #32368, #12301, #28014, .T. ) ;
#19279=CARTESIAN_POINT ( 'NONE',  ( 0.000000000000000000, 0.000000000000000000, 0.000000000000000000 ) ) ;
#19300=CARTESIAN_POINT ( 'NONE',  ( -25.25629716696160543, -17.17253483735098030, -16.29170001372755650 ) ) ;
#19343=B_SPLINE_CURVE_WITH_KNOTS ( 'NONE', 3,
 ( #6751, #27525, #24983, #1634, #20542, #17993, #25312, #12706 ),
 .UNSPECIFIED., .F., .F.,
 ( 4, 2, 2, 4 ),
 ( 0.04438889715320012974, 0.04840678451617883016, 0.05242467187915753057, 0.06046044660511493835 ),
 .UNSPECIFIED. ) ;
#19411=ORIENTED_EDGE ( 'NONE', *, *, #28019, .F. ) ;
#19456=CARTESIAN_POINT ( 'NONE',  ( 5.541103744621880989E-15, 31.75426480542943608, -18.00000000000000000 ) ) ;
#19457=( GEOMETRIC_REPRESENTATION_CONTEXT ( 3 ) GLOBAL_UNCERTAINTY_ASSIGNED_CONTEXT ( ( #7966 ) ) GLOBAL_UNIT_ASSIGNED_CONTEXT ( ( #24310, #21757, #15274 ) ) REPRESENTATION_CONTEXT ( 'NONE', 'WORKASPACE' ) );
#19466=CARTESIAN_POINT ( 'NONE',  ( -27.50000000000000000, -15.87713240271474824, -15.54379906938135214 ) ) ;
#19471=CARTESIAN_POINT ( 'NONE',  ( 0.000000000000000000, 0.000000000000000000, -1.400415076419418092 ) ) ;
#19488=EDGE_CURVE ( 'NONE', #8582, #16783, #2420, .T. ) ;
#19606=DIRECTION ( 'NONE',  ( -0.000000000000000000, -0.000000000000000000, 1.000000000000000000 ) ) ;
#19641=B_SPLINE_CURVE_WITH_KNOTS ( 'NONE', 3,
 ( #27572, #1020, #24523, #4072, #3740, #32184 ),
 .UNSPECIFIED., .F., .F.,
 ( 4, 2, 4 ),
 ( 2.380727408984196306E-07, 0.008032766472079773054, 0.01606529487141864984 ),
 .UNSPECIFIED. ) ;
#19645=ORIENTED_EDGE ( 'NONE', *, *, #31660, .T. ) ;
#19684=CARTESIAN_POINT ( 'NONE',  ( 13.75000000000000888, -23.81569860407206463, -18.00000000000000000 ) ) ;
#19786=CARTESIAN_POINT ( 'NONE',  ( 27.50000000000000355, 0.000000000000000000, -18.00000000000000000 ) ) ;
#19821=CARTESIAN_POINT ( 'NONE',  ( -22.99387487948482089, -18.47874495404631290, -1.090893241169168748 ) ) ;
#19859=CARTESIAN_POINT ( 'NONE',  ( 0.000000000000000000, 0.000000000000000000, 0.000000000000000000 ) ) ;
#19949=CARTESIAN_POINT ( 'NONE',  ( 27.50000000000001776, -15.87713240271472870, -2.456200930618646971 ) ) ;
#19985=FACE_OUTER_BOUND ( 'NONE', #25723, .T. ) ;
#20008=CARTESIAN_POINT ( 'NONE',  ( -27.50000000000000711, -5.348566131067991947, -17.76938258631346912 ) ) ;
#20084=FACE_OUTER_BOUND ( 'NONE', #4813, .T. ) ;
#20166=CARTESIAN_POINT ( 'NONE',  ( -10.83124253962819949, 25.50084400951695329, -0.1142222407377227189 ) ) ;
#20182=CARTESIAN_POINT ( 'NONE',  ( -11.40740920524442004, -25.16819403002536859, -17.99999999999998579 ) ) ;
#20263=ORIENTED_EDGE ( 'NONE', *, *, #19488, .T. ) ;
#20324=CARTESIAN_POINT ( 'NONE',  ( 13.75000000000000888, -23.81569860407206463, 0.000000000000000000 ) ) ;
#20394=ORIENTED_EDGE ( 'NONE', *, *, #21184, .T. ) ;
#20400=ORIENTED_EDGE ( 'NONE', *, *, #5018, .F. ) ;
#20410=CARTESIAN_POINT ( 'NONE',  ( 0.000000000000000000, 0.000000000000000000, 0.000000000000000000 ) ) ;
#20461=FACE_OUTER_BOUND ( 'NONE', #13853, .T. ) ;
#20487=ORIENTED_EDGE ( 'NONE', *, *, #7878, .T. ) ;
#20522=ORIENTED_EDGE ( 'NONE', *, *, #26650, .F. ) ;
#20542=CARTESIAN_POINT ( 'NONE',  ( 27.50000000000000000, 6.731471899275976334, -17.54777384619328018 ) ) ;
#20581=CIRCLE ( 'NONE', #993, 16.00000000000000000 ) ;
#20678=CARTESIAN_POINT ( 'NONE',  ( 27.50000000000000355, 0.000000000000000000, 0.000000000000000000 ) ) ;
#20714=FACE_OUTER_BOUND ( 'NONE', #8931, .T. ) ;
#20725=APPLICATION_CONTEXT ( 'automotive_design' ) ;
#20818=EDGE_CURVE ( 'NONE', #355, #25250, #1794, .T. ) ;
#20837=CARTESIAN_POINT ( 'NONE',  ( 27.50000000000000000, 6.731471899275977222, -0.4522261538067141595 ) ) ;
#20850=ORIENTED_EDGE ( 'NONE', *, *, #7878, .F. ) ;
#20855=B_SPLINE_CURVE_WITH_KNOTS ( 'NONE', 3,
 ( #8033, #21295, #18417, #31689, #3399, #13794, #24188, #21627, #32020, #27077 ),
 .UNSPECIFIED., .F., .F.,
 ( 4, 2, 2, 2, 4 ),
 ( 0.01606529487141860474, 0.01806591702017404724, 0.02006653916892948974, 0.02406778346644037475, 0.03207027206146215170 ),
 .UNSPECIFIED. ) ;
#20913=CARTESIAN_POINT ( 'NONE',  ( 22.99387487948479603, 18.47874495404627382, -16.90910675883083414 ) ) ;
#21011=ADVANCED_FACE ( 'NONE', ( #15617 ), #2371, .T. ) ;
#21063=VECTOR ( 'NONE', #6378, 1000.000000000000000 ) ;
#21106=CIRCLE ( 'NONE', #24366, 27.50000000000000355 ) ;
#21124=CARTESIAN_POINT ( 'NONE',  ( 0.000000000000000000, 0.000000000000000000, -18.00000000000000000 ) ) ;
#21162=CARTESIAN_POINT ( 'NONE',  ( 27.50000000000000355, 15.87713240271474291, -2.456200930618646971 ) ) ;
#21171=DIRECTION ( 'NONE',  ( 0.000000000000000000, -0.000000000000000000, 1.000000000000000000 ) ) ;
#21184=EDGE_CURVE ( 'NONE', #11757, #32368, #8866, .T. ) ;
#21190=ORIENTED_EDGE ( 'NONE', *, *, #27285, .F. ) ;
#21261=VECTOR ( 'NONE', #28633, 1000.000000000000000 ) ;
#21276=UNCERTAINTY_MEASURE_WITH_UNIT (LENGTH_MEASURE( 1.000000000000000082E-05 ), #26679, 'distance_accuracy_value', 'NONE');
#21295=CARTESIAN_POINT ( 'NONE',  ( -13.16654248868335664, 24.15255795529144933, -18.00000000000000711 ) ) ;
#21404=FILL_AREA_STYLE_COLOUR ( '', #263 ) ;
#21517=CARTESIAN_POINT ( 'NONE',  ( -19.55945325266601031, -20.46160920480082623, -17.55088044235631983 ) ) ;
#21563=FILL_AREA_STYLE ('',( #21404 ) ) ;
#21613=COLOUR_RGB ( '', 0.31764706, 0.68627451, 0.89019608) ;
#21627=CARTESIAN_POINT ( 'NONE',  ( -4.506125120515186211, 29.15265225409784478, -16.90910675883083414 ) ) ;
#21639=AXIS2_PLACEMENT_3D ( 'NONE', #20410, #30634, #18192 ) ;
#21666=CARTESIAN_POINT ( 'NONE',  ( 27.50000000000000355, -10.64700562007355344, -16.86587997430611807 ) ) ;
#21674=CARTESIAN_POINT ( 'NONE',  ( 0.000000000000000000, 0.000000000000000000, -18.00000000000000000 ) ) ;
#21688=VERTEX_POINT ( 'NONE', #25099 ) ;
#21757=( NAMED_UNIT ( * ) PLANE_ANGLE_UNIT ( ) SI_UNIT ( $, .RADIAN. ) );
#21848=CARTESIAN_POINT ( 'NONE',  ( -22.99387487948482089, -18.47874495404630935, -16.90910675883082703 ) ) ;
#21851=EDGE_CURVE ( 'NONE', #23832, #8655, #16303, .T. ) ;
#21887=PRODUCT_DEFINITION_FORMATION_WITH_SPECIFIED_SOURCE ( 'ANY', '', #29822, .NOT_KNOWN. ) ;
#21947=B_SPLINE_CURVE_WITH_KNOTS ( 'NONE', 3,
 ( #10477, #33635, #18132, #17789, #4845, #25625, #17969, #28531, #5180, #25962 ),
 .UNSPECIFIED., .F., .F.,
 ( 4, 2, 2, 2, 4 ),
 ( 0.01606529487141860127, 0.01806591702017404724, 0.02006653916892948974, 0.02406778346644038169, 0.03207027206146215170 ),
 .UNSPECIFIED. ) ;
#21981=ORIENTED_EDGE ( 'NONE', *, *, #4121, .T. ) ;
#22011=CARTESIAN_POINT ( 'NONE',  ( 0.000000000000000000, 0.000000000000000000, -18.00000000000000000 ) ) ;
#22023=PLANE ( 'NONE',  #25756 ) ;
#22027=DIRECTION ( 'NONE',  ( -0.000000000000000000, -0.000000000000000000, 1.000000000000000000 ) ) ;
#22049=EDGE_CURVE ( 'NONE', #7505, #7334, #30254, .T. ) ;
#22155=CARTESIAN_POINT ( 'NONE',  ( -16.09259079475562970, 22.46320317811876421, 1.931235119739804773E-15 ) ) ;
#22188=CARTESIAN_POINT ( 'NONE',  ( 18.00000000000000000, 0.000000000000000000, 3.252606517456513302E-15 ) ) ;
#22206=CARTESIAN_POINT ( 'NONE',  ( 0.000000000000000000, 0.000000000000000000, -18.00000000000000000 ) ) ;
#22288=ADVANCED_FACE ( 'NONE', ( #16388 ), #2001, .T. ) ;
#22314=CARTESIAN_POINT ( 'NONE',  ( 16.00000000000000000, 0.000000000000000000, -1.400415076419418092 ) ) ;
#22318=LINE ( 'NONE', #24715, #13986 ) ;
#22331=CIRCLE ( 'NONE', #12563, 27.50000000000000355 ) ;
#22336=LINE ( 'NONE', #14835, #27103 ) ;
#22343=ORIENTED_EDGE ( 'NONE', *, *, #3635, .F. ) ;
#22370=CARTESIAN_POINT ( 'NONE',  ( -27.50000000000000000, -13.28298644054430966, -1.741296657551681948 ) ) ;
#22379=CIRCLE ( 'NONE', #32172, 27.50000000000000355 ) ;
#22466=AXIS2_PLACEMENT_3D ( 'NONE', #26021, #22027, #14191 ) ;
#22487=AXIS2_PLACEMENT_3D ( 'NONE', #9427, #15041, #17430 ) ;
#22493=AXIS2_PLACEMENT_3D ( 'NONE', #19456, #25244, #3949 ) ;
#22495=VERTEX_POINT ( 'NONE', #7025 ) ;
#22517=CONICAL_SURFACE ( 'NONE', #23054, 27.50000000000000355, 1.047197551196595411 ) ;
#22558=CARTESIAN_POINT ( 'NONE',  ( -4.506125120515189764, 29.15265225409785543, -1.090893241169164529 ) ) ;
#22572=CARTESIAN_POINT ( 'NONE',  ( -13.75000000000001243, -23.81569860407206107, -18.00000000000000000 ) ) ;
#22586=DIRECTION ( 'NONE',  ( -1.000000000000000000, 0.000000000000000000, 0.000000000000000000 ) ) ;
#22649=EDGE_LOOP ( 'NONE', ( #10016, #31123, #16861, #6816, #20850, #29474 ) ) ;
#22650=CIRCLE ( 'NONE', #32980, 27.50000000000000355 ) ;
#22663=DIRECTION ( 'NONE',  ( 0.000000000000000000, 0.000000000000000000, -1.000000000000000000 ) ) ;
#22673=CARTESIAN_POINT ( 'NONE',  ( -4.336808689942017736E-14, -31.75426480542944319, -2.456200930618646971 ) ) ;
#22729=CARTESIAN_POINT ( 'NONE',  ( -18.00000000000000355, 2.204364238465235822E-15, -18.00000000000000000 ) ) ;
#22734=VERTEX_POINT ( 'NONE', #31208 ) ;
#22740=PLANE ( 'NONE',  #902 ) ;
#22757=CIRCLE ( 'NONE', #14036, 16.00000000000000000 ) ;
#22796=AXIS2_PLACEMENT_3D ( 'NONE', #14155, #29663, #24721 ) ;
#22883=CARTESIAN_POINT ( 'NONE',  ( -25.25629716696160543, -17.17253483735097674, -1.708299986272441284 ) ) ;
#22957=DIRECTION ( 'NONE',  ( 0.000000000000000000, 0.000000000000000000, -1.000000000000000000 ) ) ;
#22968=CIRCLE ( 'NONE', #15817, 27.50000000000000355 ) ;
#23011=SHAPE_DEFINITION_REPRESENTATION ( #32809, #16299 ) ;
#23014=DIRECTION ( 'NONE',  ( 0.000000000000000000, -0.000000000000000000, 1.000000000000000000 ) ) ;
#23054=AXIS2_PLACEMENT_3D ( 'NONE', #32004, #13442, #26551 ) ;
#23116=CARTESIAN_POINT ( 'NONE',  ( 27.50000000000000355, 0.000000000000000000, 0.000000000000000000 ) ) ;
#23133=DIRECTION ( 'NONE',  ( 1.000000000000000000, 0.000000000000000000, 0.000000000000000000 ) ) ;
#23135=CARTESIAN_POINT ( 'NONE',  ( 13.75000000000002487, 23.81569860407205397, 0.000000000000000000 ) ) ;
#23202=B_SPLINE_CURVE_WITH_KNOTS ( 'NONE', 3,
 ( #14535, #24937, #22370, #23223, #31072, #62, #8226, #33618 ),
 .UNSPECIFIED., .F., .F.,
 ( 4, 2, 2, 4 ),
 ( 0.02832689070575898985, 0.03234239231761927569, 0.03635789392947955806, 0.04438889715320012280 ),
 .UNSPECIFIED. ) ;
#23223=CARTESIAN_POINT ( 'NONE',  ( -27.50000000000000000, -10.64700562007355344, -1.134120025693880596 ) ) ;
#23301=CARTESIAN_POINT ( 'NONE',  ( 19.55945325266599966, 20.46160920480081202, -17.55088044235633760 ) ) ;
#23371=ORIENTED_EDGE ( 'NONE', *, *, #20818, .F. ) ;
#23384=CIRCLE ( 'NONE', #11943, 27.50000000000000355 ) ;
#23399=CARTESIAN_POINT ( 'NONE',  ( 18.40782811468575275, 21.12650028821923343, -0.2827231011780743652 ) ) ;
#23415=ORIENTED_EDGE ( 'NONE', *, *, #6166, .T. ) ;
#23463=CARTESIAN_POINT ( 'NONE',  ( 0.000000000000000000, 0.000000000000000000, 0.000000000000000000 ) ) ;
#23466=CARTESIAN_POINT ( 'NONE',  ( 14.91983402814537740, 23.14029461301515056, -17.98559444045776701 ) ) ;
#23568=APPLICATION_CONTEXT ( 'automotive_design' ) ;
#23635=SURFACE_STYLE_USAGE ( .BOTH. , #7974 ) ;
#23701=ORIENTED_EDGE ( 'NONE', *, *, #3635, .T. ) ;
#23703=CARTESIAN_POINT ( 'NONE',  ( 4.506125120515186211, -29.15265225409787675, -16.90910675883081637 ) ) ;
#23715=ADVANCED_FACE ( 'NONE', ( #980 ), #7456, .F. ) ;
#23722=CARTESIAN_POINT ( 'NONE',  ( 16.08713178458080861, 22.46635493911270132, -0.07154745401828326024 ) ) ;
#23754=CARTESIAN_POINT ( 'NONE',  ( -4.336808689942017736E-14, -31.75426480542944319, -2.456200930618646971 ) ) ;
#23786=CONICAL_SURFACE ( 'NONE', #29232, 18.00000000000000711, 0.9599310885968802554 ) ;
#23813=MANIFOLD_SOLID_BREP ( 'EndChamfer', #30281 ) ;
#23832=VERTEX_POINT ( 'NONE', #23116 ) ;
#23854=EDGE_LOOP ( 'NONE', ( #8780, #26672 ) ) ;
#23864=VERTEX_POINT ( 'NONE', #10176 ) ;
#23896=DIRECTION ( 'NONE',  ( -1.000000000000000000, 0.000000000000000000, 0.000000000000000000 ) ) ;
#23898=ADVANCED_FACE ( 'NONE', ( #33339 ), #23786, .F. ) ;
#23911=CARTESIAN_POINT ( 'NONE',  ( 7.331804101520335523E-16, -31.75426480542945740, -18.00000000000000000 ) ) ;
#23925=CARTESIAN_POINT ( 'NONE',  ( 27.50000000000000000, -14.58598892539967906, -2.083479913523504923 ) ) ;
#24037=ORIENTED_EDGE ( 'NONE', *, *, #7473, .T. ) ;
#24117=AXIS2_PLACEMENT_3D ( 'NONE', #32243, #459, #28902 ) ;
#24174=FACE_OUTER_BOUND ( 'NONE', #15778, .T. ) ;
#24188=CARTESIAN_POINT ( 'NONE',  ( -7.940546747334008337, 27.16978800334332078, -17.55088044235632694 ) ) ;
#24282=ADVANCED_FACE ( 'NONE', ( #13889 ), #16945, .T. ) ;
#24291=VECTOR ( 'NONE', #8825, 1000.000000000000000 ) ;
#24295=CARTESIAN_POINT ( 'NONE',  ( 0.000000000000000000, 0.000000000000000000, 0.000000000000000000 ) ) ;
#24310=( LENGTH_UNIT ( ) NAMED_UNIT ( * ) SI_UNIT ( .MILLI., .METRE. ) );
#24337=AXIS2_PLACEMENT_3D ( 'NONE', #1117, #8950, #1618 ) ;
#24345=CARTESIAN_POINT ( 'NONE',  ( 0.000000000000000000, 0.000000000000000000, -1.400415076419418092 ) ) ;
#24349=EDGE_CURVE ( 'NONE', #31055, #18759, #13472, .T. ) ;
#24366=AXIS2_PLACEMENT_3D ( 'NONE', #28544, #7756, #10324 ) ;
#24415=CARTESIAN_POINT ( 'NONE',  ( -13.75000000000001243, -23.81569860407206107, -18.00000000000000000 ) ) ;
#24486=DIRECTION ( 'NONE',  ( -0.000000000000000000, -0.000000000000000000, 1.000000000000000000 ) ) ;
#24492=EDGE_CURVE ( 'NONE', #16783, #32368, #1640, .T. ) ;
#24523=CARTESIAN_POINT ( 'NONE',  ( 4.515071337844632104, 29.14748715311447924, -16.91127448208919049 ) ) ;
#24618=CARTESIAN_POINT ( 'NONE',  ( 16.00000000000000000, 0.000000000000000000, -16.57418492358057094 ) ) ;
#24642=CARTESIAN_POINT ( 'NONE',  ( -27.50000000000000000, 2.688867821578071471, -17.94295719123740085 ) ) ;
#24659=FILL_AREA_STYLE_COLOUR ( '', #21613 ) ;
#24679=AXIS2_PLACEMENT_3D ( 'NONE', #23911, #26300, #31742 ) ;
#24696=CARTESIAN_POINT ( 'NONE',  ( 27.50000000000000355, 15.87713240271474291, -2.456200930618646971 ) ) ;
#24709=ORIENTED_EDGE ( 'NONE', *, *, #4975, .T. ) ;
#24715=CARTESIAN_POINT ( 'NONE',  ( -18.00000000000000355, 2.204364238465235822E-15, -25.03750572909317285 ) ) ;
#24721=DIRECTION ( 'NONE',  ( 0.000000000000000000, 0.000000000000000000, 1.000000000000000000 ) ) ;
#24735=CARTESIAN_POINT ( 'NONE',  ( 16.09259079475563325, -22.46320317811879264, -1.422337725029421129E-14 ) ) ;
#24741=CARTESIAN_POINT ( 'NONE',  ( 18.00000000000000355, 0.000000000000000000, -25.03750572909317285 ) ) ;
#24755=ORIENTED_EDGE ( 'NONE', *, *, #13543, .T. ) ;
#24808=DIRECTION ( 'NONE',  ( -0.8191520442889912434, 0.000000000000000000, -0.5735764363510469366 ) ) ;
#24906=PLANE ( 'NONE',  #22493 ) ;
#24910=AXIS2_PLACEMENT_3D ( 'NONE', #23463, #22957, #9847 ) ;
#24934=CARTESIAN_POINT ( 'NONE',  ( -16.08713178458081217, -22.46635493911272619, -0.07154745401829776252 ) ) ;
#24937=CARTESIAN_POINT ( 'NONE',  ( -27.49999999999999289, -14.58598892539970215, -2.083479913523507587 ) ) ;
#24983=CARTESIAN_POINT ( 'NONE',  ( 27.50000000000000355, 2.688867821578065698, -17.94295719123739730 ) ) ;
#24999=VERTEX_POINT ( 'NONE', #22314 ) ;
#25013=DIRECTION ( 'NONE',  ( -0.8191520442889912434, 1.003171929053524007E-16, 0.5735764363510469366 ) ) ;
#25031=CARTESIAN_POINT ( 'NONE',  ( 0.000000000000000000, 0.000000000000000000, -1.540456584061364431 ) ) ;
#25099=CARTESIAN_POINT ( 'NONE',  ( -13.75000000000001954, 23.81569860407205752, 0.000000000000000000 ) ) ;
#25136=LINE ( 'NONE', #1800, #12132 ) ;
#25244=DIRECTION ( 'NONE',  ( -0.5000000000000006661, 0.8660254037844382635, 0.000000000000000000 ) ) ;
#25250=VERTEX_POINT ( 'NONE', #4763 ) ;
#25312=CARTESIAN_POINT ( 'NONE',  ( 27.50000000000001066, 13.30988860919481986, -16.28489851701342417 ) ) ;
#25401=CIRCLE ( 'NONE', #27021, 16.00000000000000000 ) ;
#25458=FACE_OUTER_BOUND ( 'NONE', #11750, .T. ) ;
#25469=ORIENTED_EDGE ( 'NONE', *, *, #1901, .T. ) ;
#25470=DIRECTION ( 'NONE',  ( -1.000000000000000000, 0.000000000000000000, 0.000000000000000000 ) ) ;
#25514=CARTESIAN_POINT ( 'NONE',  ( 25.25629716696158411, 17.17253483735094832, -16.29170001372757071 ) ) ;
#25612=CARTESIAN_POINT ( 'NONE',  ( 27.50000000000000355, 15.87713240271474291, -2.456200930618646971 ) ) ;
#25625=CARTESIAN_POINT ( 'NONE',  ( 9.092171885314265012, -26.50489691992491714, -0.2827231011780930725 ) ) ;
#25684=CARTESIAN_POINT ( 'NONE',  ( 14.33345751131667889, 23.47883925285266571, -18.00000000000000000 ) ) ;
#25723=EDGE_LOOP ( 'NONE', ( #4148, #20487, #32822 ) ) ;
#25756=AXIS2_PLACEMENT_3D ( 'NONE', #8577, #32240, #14360 ) ;
#25760=CARTESIAN_POINT ( 'NONE',  ( 2.243702833038388356, -30.45886237079322356, -16.29170001372754228 ) ) ;
#25799=AXIS2_PLACEMENT_3D ( 'NONE', #26971, #3633, #15913 ) ;
#25855=FACE_OUTER_BOUND ( 'NONE', #13891, .T. ) ;
#25944=CARTESIAN_POINT ( 'NONE',  ( 0.000000000000000000, 0.000000000000000000, -18.00000000000000000 ) ) ;
#25962=CARTESIAN_POINT ( 'NONE',  ( -4.336808689942017736E-14, -31.75426480542944319, -2.456200930618646971 ) ) ;
#25963=ADVANCED_FACE ( 'NONE', ( #28579 ), #11873, .F. ) ;
#26021=CARTESIAN_POINT ( 'NONE',  ( 0.000000000000000000, 0.000000000000000000, -18.00000000000000000 ) ) ;
#26028=CARTESIAN_POINT ( 'NONE',  ( 15.79999999999999538, 0.000000000000000000, -1.540456584061364431 ) ) ;
#26030=CONICAL_SURFACE ( 'NONE', #14587, 27.50000000000000355, 1.047197551196595411 ) ;
#26071=DIRECTION ( 'NONE',  ( 0.000000000000000000, 0.000000000000000000, -1.000000000000000000 ) ) ;
#26081=DIRECTION ( 'NONE',  ( -0.000000000000000000, -0.000000000000000000, 1.000000000000000000 ) ) ;
#26092=ORIENTED_EDGE ( 'NONE', *, *, #8640, .F. ) ;
#26131=VERTEX_POINT ( 'NONE', #8134 ) ;
#26152=CARTESIAN_POINT ( 'NONE',  ( 27.50000000000000000, -9.324699302609159801, -0.8718021930569386235 ) ) ;
#26168=VERTEX_POINT ( 'NONE', #19015 ) ;
#26174=ORIENTED_EDGE ( 'NONE', *, *, #12482, .F. ) ;
#26203=CONICAL_SURFACE ( 'NONE', #12044, 27.50000000000000355, 1.047197551196595411 ) ;
#26234=CARTESIAN_POINT ( 'NONE',  ( -18.40606158072672116, 21.12752019707600937, -17.76591125084755873 ) ) ;
#26259=CARTESIAN_POINT ( 'NONE',  ( -9.093938419273312590, -26.50387701106812344, -17.76591125084755163 ) ) ;
#26260=CARTESIAN_POINT ( 'NONE',  ( -4.336808689942017736E-14, -31.75426480542944319, -15.54379906938135214 ) ) ;
#26285=CARTESIAN_POINT ( 'NONE',  ( 0.000000000000000000, 0.000000000000000000, 0.000000000000000000 ) ) ;
#26300=DIRECTION ( 'NONE',  ( 0.5000000000000003331, -0.8660254037844384856, 0.000000000000000000 ) ) ;
#26416=CARTESIAN_POINT ( 'NONE',  ( -4.336808689942017736E-14, -31.75426480542944319, -15.54379906938135214 ) ) ;
#26477=AXIS2_PLACEMENT_3D ( 'NONE', #27039, #24486, #4201 ) ;
#26498=VERTEX_POINT ( 'NONE', #29574 ) ;
#26551=DIRECTION ( 'NONE',  ( -1.000000000000000000, 0.000000000000000000, 0.000000000000000000 ) ) ;
#26586=EDGE_CURVE ( 'NONE', #17155, #22495, #25401, .T. ) ;
#26627=CARTESIAN_POINT ( 'NONE',  ( -14.91983402814538451, -23.14029461301517543, -17.98559444045775280 ) ) ;
#26649=LINE ( 'NONE', #24741, #16805 ) ;
#26650=EDGE_CURVE ( 'NONE', #22495, #17155, #28693, .T. ) ;
#26672=ORIENTED_EDGE ( 'NONE', *, *, #22049, .T. ) ;
#26678=CARTESIAN_POINT ( 'NONE',  ( 2.249320974685011798, 30.45561873520116691, -1.706427272390174776 ) ) ;
#26679=( LENGTH_UNIT ( ) NAMED_UNIT ( * ) SI_UNIT ( .MILLI., .METRE. ) );
#26687=CARTESIAN_POINT ( 'NONE',  ( -27.50000000000000355, 5.390523180938865622, -17.71625836475402238 ) ) ;
#26724=B_SPLINE_CURVE_WITH_KNOTS ( 'NONE', 3,
 ( #5821, #16718, #16885, #21666, #13658, #16216, #1218, #26945 ),
 .UNSPECIFIED., .F., .F.,
 ( 4, 2, 2, 4 ),
 ( 0.02832689070575900372, 0.03234239231761928957, 0.03635789392947956500, 0.04438889715320012974 ),
 .UNSPECIFIED. ) ;
#26737=CARTESIAN_POINT ( 'NONE',  ( 13.75000000000000888, -23.81569860407206463, -18.00000000000000000 ) ) ;
#26873=SURFACE_STYLE_USAGE ( .BOTH. , #17152 ) ;
#26911=DIRECTION ( 'NONE',  ( -1.000000000000000000, 0.000000000000000000, 0.000000000000000000 ) ) ;
#26945=CARTESIAN_POINT ( 'NONE',  ( 27.50000000000000355, 0.000000000000000000, -18.00000000000000000 ) ) ;
#26971=CARTESIAN_POINT ( 'NONE',  ( 0.000000000000000000, 0.000000000000000000, 3.469446951953614189E-15 ) ) ;
#27021=AXIS2_PLACEMENT_3D ( 'NONE', #30585, #7249, #7758 ) ;
#27024=CARTESIAN_POINT ( 'NONE',  ( -27.50000000000000000, 0.000000000000000000, -18.00000000000000000 ) ) ;
#27039=CARTESIAN_POINT ( 'NONE',  ( 0.000000000000000000, 0.000000000000000000, -1.540456584061364431 ) ) ;
#27077=CARTESIAN_POINT ( 'NONE',  ( 1.734723475976807094E-14, 31.75426480542944319, -15.54379906938135214 ) ) ;
#27103=VECTOR ( 'NONE', #12457, 1000.000000000000000 ) ;
#27135=EDGE_LOOP ( 'NONE', ( #18563, #26174, #3124 ) ) ;
#27179=CARTESIAN_POINT ( 'NONE',  ( 0.000000000000000000, 0.000000000000000000, 0.000000000000000000 ) ) ;
#27285=EDGE_CURVE ( 'NONE', #26168, #23832, #2000, .T. ) ;
#27302=ORIENTED_EDGE ( 'NONE', *, *, #6565, .T. ) ;
#27442=EDGE_CURVE ( 'NONE', #17155, #24999, #29378, .T. ) ;
#27494=CARTESIAN_POINT ( 'NONE',  ( -7.940546747334013666, 27.16978800334332433, -0.4491195576436714521 ) ) ;
#27502=CARTESIAN_POINT ( 'NONE',  ( -27.50000000000000355, -10.64700562007355344, -16.86587997430611807 ) ) ;
#27504=DIRECTION ( 'NONE',  ( 0.8660254037844383745, -0.5000000000000004441, 0.000000000000000000 ) ) ;
#27524=CARTESIAN_POINT ( 'NONE',  ( -18.00000000000000711, 0.000000000000000000, -17.97459999999999525 ) ) ;
#27525=CARTESIAN_POINT ( 'NONE',  ( 27.50000000000000000, 1.342284157770883724, -18.00000000000000000 ) ) ;
#27572=CARTESIAN_POINT ( 'NONE',  ( 1.734723475976807094E-14, 31.75426480542944319, -15.54379906938135214 ) ) ;
#27587=ORIENTED_EDGE ( 'NONE', *, *, #9111, .T. ) ;
#27591=EDGE_CURVE ( 'NONE', #30720, #19012, #5841, .T. ) ;
#27599=DIRECTION ( 'NONE',  ( 0.000000000000000000, 0.000000000000000000, 1.000000000000000000 ) ) ;
#27660=ORIENTED_EDGE ( 'NONE', *, *, #24492, .T. ) ;
#27720=ORIENTED_EDGE ( 'NONE', *, *, #7946, .T. ) ;
#27732=CARTESIAN_POINT ( 'NONE',  ( 0.000000000000000000, 0.000000000000000000, 0.000000000000000000 ) ) ;
#27764=DIRECTION ( 'NONE',  ( -1.000000000000000000, 0.000000000000000000, 0.000000000000000000 ) ) ;
#27770=LINE ( 'NONE', #4615, #496 ) ;
#27793=EDGE_CURVE ( 'NONE', #17333, #26168, #30733, .T. ) ;
#27874=DIRECTION ( 'NONE',  ( 0.000000000000000000, 0.000000000000000000, -1.000000000000000000 ) ) ;
#27895=( NAMED_UNIT ( * ) SI_UNIT ( $, .STERADIAN. ) SOLID_ANGLE_UNIT ( ) );
#27937=FACE_OUTER_BOUND ( 'NONE', #27135, .T. ) ;
#27954=CARTESIAN_POINT ( 'NONE',  ( -2.249320974685042440, -30.45561873520117757, -1.706427272390177663 ) ) ;
#27998=CARTESIAN_POINT ( 'NONE',  ( 27.50000000000000355, 1.342284157770885500, -7.623296525288699970E-18 ) ) ;
#28014=B_SPLINE_CURVE_WITH_KNOTS ( 'NONE', 3,
 ( #24415, #1080, #26627, #9071, #11469, #3290, #21517, #21848, #19300, #19466 ),
 .UNSPECIFIED., .F., .F.,
 ( 4, 2, 2, 2, 4 ),
 ( 0.01606529487141865678, 0.01806591702017409581, 0.02006653916892953138, 0.02406778346644039210, 0.03207027206146211701 ),
 .UNSPECIFIED. ) ;
#28019=EDGE_CURVE ( 'NONE', #1785, #253, #12968, .T. ) ;
#28020=ORIENTED_EDGE ( 'NONE', *, *, #3972, .T. ) ;
#28068=CARTESIAN_POINT ( 'NONE',  ( 27.50000000000000355, 15.87713240271474291, -15.54379906938135214 ) ) ;
#28126=CARTESIAN_POINT ( 'NONE',  ( 25.25067902531501574, -17.17577847294299076, -1.706427272390178773 ) ) ;
#28130=EDGE_CURVE ( 'NONE', #17333, #28277, #26724, .T. ) ;
#28149=STYLED_ITEM ( 'NONE', ( #9149 ), #23813 ) ;
#28249=LINE ( 'NONE', #15290, #18308 ) ;
#28277=VERTEX_POINT ( 'NONE', #19786 ) ;
#28284=EDGE_LOOP ( 'NONE', ( #8907, #944, #1608, #13060, #3288, #9706 ) ) ;
#28376=CARTESIAN_POINT ( 'NONE',  ( -27.50000000000000355, 0.000000000000000000, 0.000000000000000000 ) ) ;
#28413=FACE_OUTER_BOUND ( 'NONE', #28731, .T. ) ;
#28469=CARTESIAN_POINT ( 'NONE',  ( -13.75000000000001954, 23.81569860407205752, -18.00000000000000000 ) ) ;
#28476=EDGE_CURVE ( 'NONE', #16783, #33588, #22336, .T. ) ;
#28493=CARTESIAN_POINT ( 'NONE',  ( 10.83124253962819949, -25.50084400951697816, -17.88577775926225399 ) ) ;
#28510=EDGE_CURVE ( 'NONE', #26168, #31055, #15785, .T. ) ;
#28531=CARTESIAN_POINT ( 'NONE',  ( 4.506125120515185323, -29.15265225409788030, -1.090893241169181183 ) ) ;
#28544=CARTESIAN_POINT ( 'NONE',  ( 0.000000000000000000, 0.000000000000000000, -18.00000000000000000 ) ) ;
#28554=CARTESIAN_POINT ( 'NONE',  ( 27.50000000000000355, -13.28298644054429545, -1.741296657551683280 ) ) ;
#28571=ORIENTED_EDGE ( 'NONE', *, *, #21851, .T. ) ;
#28579=FACE_OUTER_BOUND ( 'NONE', #33685, .T. ) ;
#28623=CARTESIAN_POINT ( 'NONE',  ( 0.000000000000000000, 0.000000000000000000, 0.000000000000000000 ) ) ;
#28633=DIRECTION ( 'NONE',  ( 0.8191520442889912434, 1.003171929053524007E-16, -0.5735764363510469366 ) ) ;
#28680=AXIS2_PLACEMENT_3D ( 'NONE', #1105, #13700, #18661 ) ;
#28693=CIRCLE ( 'NONE', #6353, 16.00000000000000000 ) ;
#28731=EDGE_LOOP ( 'NONE', ( #20522, #23701, #30455, #30449 ) ) ;
#28746=EDGE_CURVE ( 'NONE', #24999, #26131, #22757, .T. ) ;
#28775=B_SPLINE_CURVE_WITH_KNOTS ( 'NONE', 3,
 ( #15215, #9590, #33104, #24934, #2272, #14532, #30728, #19821, #22883, #7387 ),
 .UNSPECIFIED., .F., .F.,
 ( 4, 2, 2, 2, 4 ),
 ( 0.01606529487141865678, 0.01806591702017409581, 0.02006653916892953138, 0.02406778346644039557, 0.03207027206146212395 ),
 .UNSPECIFIED. ) ;
#28902=DIRECTION ( 'NONE',  ( -1.000000000000000000, 0.000000000000000000, 0.000000000000000000 ) ) ;
#28925=CIRCLE ( 'NONE', #8257, 27.50000000000000355 ) ;
#28985=ORIENTED_EDGE ( 'NONE', *, *, #6166, .F. ) ;
#29024=CARTESIAN_POINT ( 'NONE',  ( -13.75000000000001243, -23.81569860407206107, 0.000000000000000000 ) ) ;
#29056=AXIS2_PLACEMENT_3D ( 'NONE', #30861, #26081, #7525 ) ;
#29079=PRESENTATION_STYLE_ASSIGNMENT (( #23635 ) ) ;
#29162=ADVANCED_FACE ( 'NONE', ( #15638 ), #31321, .F. ) ;
#29196=VECTOR ( 'NONE', #10198, 1000.000000000000000 ) ;
#29216=CARTESIAN_POINT ( 'NONE',  ( -27.50000000000000000, -15.87713240271473225, -18.00000000000000000 ) ) ;
#29232=AXIS2_PLACEMENT_3D ( 'NONE', #7447, #27874, #4551 ) ;
#29269=ORIENTED_EDGE ( 'NONE', *, *, #2334, .T. ) ;
#29305=ORIENTED_EDGE ( 'NONE', *, *, #4127, .T. ) ;
#29338=CONICAL_SURFACE ( 'NONE', #32587, 27.50000000000000355, 1.047197551196595411 ) ;
#29378=LINE ( 'NONE', #8925, #9102 ) ;
#29393=CYLINDRICAL_SURFACE ( 'NONE', #14825, 16.00000000000000000 ) ;
#29446=CARTESIAN_POINT ( 'NONE',  ( 5.541103744621880989E-15, 31.75426480542943608, -18.00000000000000000 ) ) ;
#29474=ORIENTED_EDGE ( 'NONE', *, *, #4832, .F. ) ;
#29574=CARTESIAN_POINT ( 'NONE',  ( -13.75000000000001954, 23.81569860407205752, -18.00000000000000000 ) ) ;
#29629=( GEOMETRIC_REPRESENTATION_CONTEXT ( 3 ) GLOBAL_UNCERTAINTY_ASSIGNED_CONTEXT ( ( #3176 ) ) GLOBAL_UNIT_ASSIGNED_CONTEXT ( ( #18194, #33522, #27895 ) ) REPRESENTATION_CONTEXT ( 'NONE', 'WORKASPACE' ) );
#29643=ORIENTED_EDGE ( 'NONE', *, *, #6565, .F. ) ;
#29663=DIRECTION ( 'NONE',  ( -1.000000000000000000, 0.000000000000000000, 0.000000000000000000 ) ) ;
#29684=VERTEX_POINT ( 'NONE', #16802 ) ;
#29822=PRODUCT ( 'hex thin nut chamfered gradeab_iso_ISO - 4035 - M36 - N', 'hex thin nut chamfered gradeab_iso_ISO - 4035 - M36 - N', '', ( #31352 ) ) ;
#29879=CARTESIAN_POINT ( 'NONE',  ( -18.00000000000000000, 2.204364238465235428E-15, 3.252606517456513302E-15 ) ) ;
#29885=DIRECTION ( 'NONE',  ( 0.000000000000000000, 0.000000000000000000, 1.000000000000000000 ) ) ;
#29923=ADVANCED_FACE ( 'NONE', ( #20714 ), #15164, .T. ) ;
#29970=EDGE_CURVE ( 'NONE', #7334, #25250, #26649, .T. ) ;
#30003=CARTESIAN_POINT ( 'NONE',  ( -27.50000000000000000, 0.000000000000000000, -18.00000000000000000 ) ) ;
#30110=ORIENTED_EDGE ( 'NONE', *, *, #22049, .F. ) ;
#30165=ORIENTED_EDGE ( 'NONE', *, *, #33090, .F. ) ;
#30193=ORIENTED_EDGE ( 'NONE', *, *, #17926, .T. ) ;
#30254=CIRCLE ( 'NONE', #5311, 18.00000000000000355 ) ;
#30281=CLOSED_SHELL ( 'NONE', ( #12702, #25963, #32494, #10648, #17287, #16359, #24282, #1865, #18926, #27, #19107, #8818, #10026, #3907, #29923, #21011, #11005, #5970, #22288, #1196, #361, #11997, #10550, #13682, #2296, #23715, #23898, #29162 ) ) ;
#30308=DIRECTION ( 'NONE',  ( 0.000000000000000000, 0.000000000000000000, -1.000000000000000000 ) ) ;
#30330=ORIENTED_EDGE ( 'NONE', *, *, #4832, .T. ) ;
#30342=AXIS2_PLACEMENT_3D ( 'NONE', #16256, #3473, #14204 ) ;
#30348=CARTESIAN_POINT ( 'NONE',  ( 22.98492866215539365, -18.48391005502967843, -1.088725517910815066 ) ) ;
#30408=CARTESIAN_POINT ( 'NONE',  ( -27.50000000000000000, 0.000000000000000000, -18.00000000000000000 ) ) ;
#30425=CARTESIAN_POINT ( 'NONE',  ( 25.25067902531500508, -17.17577847294298721, -16.29357272760982767 ) ) ;
#30449=ORIENTED_EDGE ( 'NONE', *, *, #27442, .F. ) ;
#30455=ORIENTED_EDGE ( 'NONE', *, *, #28746, .F. ) ;
#30465=DIRECTION ( 'NONE',  ( -1.000000000000000000, 0.000000000000000000, 0.000000000000000000 ) ) ;
#30479=DIRECTION ( 'NONE',  ( 1.000000000000000000, 0.000000000000000000, 0.000000000000000000 ) ) ;
#30503=DIRECTION ( 'NONE',  ( -1.000000000000000000, 0.000000000000000000, 0.000000000000000000 ) ) ;
#30569=ORIENTED_EDGE ( 'NONE', *, *, #33554, .T. ) ;
#30571=CIRCLE ( 'NONE', #16958, 27.50000000000000355 ) ;
#30585=CARTESIAN_POINT ( 'NONE',  ( 0.000000000000000000, 0.000000000000000000, -16.57418492358057094 ) ) ;
#30634=DIRECTION ( 'NONE',  ( 0.000000000000000000, 0.000000000000000000, -1.000000000000000000 ) ) ;
#30667=ORIENTED_EDGE ( 'NONE', *, *, #7473, .F. ) ;
#30720=VERTEX_POINT ( 'NONE', #29879 ) ;
#30728=CARTESIAN_POINT ( 'NONE',  ( -19.55945325266600676, -20.46160920480082979, -0.4491195576436824433 ) ) ;
#30733=LINE ( 'NONE', #9947, #16176 ) ;
#30803=CARTESIAN_POINT ( 'NONE',  ( 13.75000000000002487, 23.81569860407205397, -18.00000000000000000 ) ) ;
#30817=DIRECTION ( 'NONE',  ( 1.000000000000000000, 0.000000000000000000, 0.000000000000000000 ) ) ;
#30861=CARTESIAN_POINT ( 'NONE',  ( 0.000000000000000000, 0.000000000000000000, -25.03750572909317285 ) ) ;
#30902=DIRECTION ( 'NONE',  ( -1.000000000000000000, -1.776356839400250465E-15, 0.000000000000000000 ) ) ;
#31055=VERTEX_POINT ( 'NONE', #20324 ) ;
#31072=CARTESIAN_POINT ( 'NONE',  ( -27.50000000000000000, -9.324699302609168683, -0.8718021930569370692 ) ) ;
#31123=ORIENTED_EDGE ( 'NONE', *, *, #13543, .F. ) ;
#31131=DIRECTION ( 'NONE',  ( 0.000000000000000000, 0.000000000000000000, -1.000000000000000000 ) ) ;
#31138=LINE ( 'NONE', #26028, #29196 ) ;
#31181=EDGE_CURVE ( 'NONE', #29684, #22734, #31554, .T. ) ;
#31208=CARTESIAN_POINT ( 'NONE',  ( 6.938893903907228378E-15, 31.75426480542944319, -2.456200930618646971 ) ) ;
#31218=CARTESIAN_POINT ( 'NONE',  ( 13.16654248868335664, -24.15255795529146710, -17.99999999999998579 ) ) ;
#31263=PRODUCT_DEFINITION ( 'UNKNOWN', '', #21887, #32239 ) ;
#31321=CYLINDRICAL_SURFACE ( 'NONE', #1008, 18.00000000000000355 ) ;
#31343=ORIENTED_EDGE ( 'NONE', *, *, #8640, .T. ) ;
#31352=PRODUCT_CONTEXT ( 'NONE', #23568, 'mechanical' ) ;
#31439=EDGE_CURVE ( 'NONE', #1785, #21688, #22650, .T. ) ;
#31448=EDGE_CURVE ( 'NONE', #26131, #30720, #28249, .T. ) ;
#31554=LINE ( 'NONE', #29446, #24291 ) ;
#31579=ORIENTED_EDGE ( 'NONE', *, *, #27591, .F. ) ;
#31660=EDGE_CURVE ( 'NONE', #24999, #19012, #31138, .T. ) ;
#31689=CARTESIAN_POINT ( 'NONE',  ( -11.41286821541921448, 25.16504226903141017, -17.92845254598170257 ) ) ;
#31718=CONICAL_SURFACE ( 'NONE', #17029, 15.79999999999999538, 0.9599310885968802554 ) ;
#31742=DIRECTION ( 'NONE',  ( 0.8660254037844384856, 0.5000000000000003331, 0.000000000000000000 ) ) ;
#31769=LINE ( 'NONE', #29216, #21063 ) ;
#31784=VERTEX_POINT ( 'NONE', #23135 ) ;
#31945=CIRCLE ( 'NONE', #28680, 18.00000000000000355 ) ;
#31956=CARTESIAN_POINT ( 'NONE',  ( 11.40740920524441293, 25.16819403002535083, 4.946672411965113980E-16 ) ) ;
#31963=CARTESIAN_POINT ( 'NONE',  ( -27.50000000000000000, 15.87713240271474824, -15.54379906938135214 ) ) ;
#32004=CARTESIAN_POINT ( 'NONE',  ( 0.000000000000000000, 0.000000000000000000, 0.000000000000000000 ) ) ;
#32020=CARTESIAN_POINT ( 'NONE',  ( -2.243702833038388356, 30.45886237079318093, -16.29170001372754939 ) ) ;
#32115=DIRECTION ( 'NONE',  ( -1.000000000000000000, 0.000000000000000000, 0.000000000000000000 ) ) ;
#32172=AXIS2_PLACEMENT_3D ( 'NONE', #25944, #2950, #30902 ) ;
#32179=B_SPLINE_CURVE_WITH_KNOTS ( 'NONE', 3,
 ( #16289, #26678, #3340, #13727, #31956, #19019 ),
 .UNSPECIFIED., .F., .F.,
 ( 4, 2, 4 ),
 ( 2.380727408881369683E-07, 0.008032766472079767850, 0.01606529487141864984 ),
 .UNSPECIFIED. ) ;
#32184=CARTESIAN_POINT ( 'NONE',  ( 13.75000000000002487, 23.81569860407205397, -18.00000000000000000 ) ) ;
#32209=CARTESIAN_POINT ( 'NONE',  ( -27.50000000000000000, 15.87713240271469672, -2.456200930618631428 ) ) ;
#32239=PRODUCT_DEFINITION_CONTEXT ( 'detailed design', #20725, 'design' ) ;
#32240=DIRECTION ( 'NONE',  ( -1.000000000000000000, 0.000000000000000000, 0.000000000000000000 ) ) ;
#32243=CARTESIAN_POINT ( 'NONE',  ( 0.000000000000000000, 0.000000000000000000, -18.00000000000000000 ) ) ;
#32343=MECHANICAL_DESIGN_GEOMETRIC_PRESENTATION_REPRESENTATION('',(#17666),#4614);
#32368=VERTEX_POINT ( 'NONE', #8683 ) ;
#32440=CARTESIAN_POINT ( 'NONE',  ( 0.000000000000000000, 0.000000000000000000, -18.00000000000000000 ) ) ;
#32478=AXIS2_PLACEMENT_3D ( 'NONE', #14996, #19606, #33227 ) ;
#32485=ORIENTED_EDGE ( 'NONE', *, *, #31448, .F. ) ;
#32494=ADVANCED_FACE ( 'NONE', ( #20084 ), #31718, .F. ) ;
#32497=ORIENTED_EDGE ( 'NONE', *, *, #12482, .T. ) ;
#32539=ORIENTED_EDGE ( 'NONE', *, *, #395, .T. ) ;
#32587=AXIS2_PLACEMENT_3D ( 'NONE', #4267, #22663, #30503 ) ;
#32595=DIRECTION ( 'NONE',  ( -0.000000000000000000, -0.000000000000000000, 1.000000000000000000 ) ) ;
#32743=CONICAL_SURFACE ( 'NONE', #2291, 27.50000000000000355, 1.047197551196595411 ) ;
#32747=DIRECTION ( 'NONE',  ( 0.000000000000000000, 0.000000000000000000, -1.000000000000000000 ) ) ;
#32804=FACE_OUTER_BOUND ( 'NONE', #3817, .T. ) ;
#32809=PRODUCT_DEFINITION_SHAPE ( 'NONE', 'NONE',  #31263 ) ;
#32822=ORIENTED_EDGE ( 'NONE', *, *, #28130, .F. ) ;
#32859=PLANE ( 'NONE',  #542 ) ;
#32885=FACE_OUTER_BOUND ( 'NONE', #9205, .T. ) ;
#32895=DIRECTION ( 'NONE',  ( -0.000000000000000000, 0.000000000000000000, -1.000000000000000000 ) ) ;
#32943=CARTESIAN_POINT ( 'NONE',  ( -13.75000000000001954, 23.81569860407205752, 0.000000000000000000 ) ) ;
#32980=AXIS2_PLACEMENT_3D ( 'NONE', #27732, #12230, #30465 ) ;
#33090=EDGE_CURVE ( 'NONE', #17333, #8582, #1945, .T. ) ;
#33104=CARTESIAN_POINT ( 'NONE',  ( -14.91983402814537740, -23.14029461301516832, -0.01440555954224943640 ) ) ;
#33182=CARTESIAN_POINT ( 'NONE',  ( 0.000000000000000000, 0.000000000000000000, -17.97459999999999525 ) ) ;
#33227=DIRECTION ( 'NONE',  ( 1.000000000000000000, 0.000000000000000000, 0.000000000000000000 ) ) ;
#33260=VECTOR ( 'NONE', #29885, 1000.000000000000000 ) ;
#33333=DIRECTION ( 'NONE',  ( -1.000000000000000000, 0.000000000000000000, 0.000000000000000000 ) ) ;
#33339=FACE_OUTER_BOUND ( 'NONE', #4939, .T. ) ;
#33461=ORIENTED_EDGE ( 'NONE', *, *, #24492, .F. ) ;
#33522=( NAMED_UNIT ( * ) PLANE_ANGLE_UNIT ( ) SI_UNIT ( $, .RADIAN. ) );
#33554=EDGE_CURVE ( 'NONE', #19012, #30720, #7295, .T. ) ;
#33574=AXIS2_PLACEMENT_3D ( 'NONE', #9211, #9538, #27764 ) ;
#33578=CARTESIAN_POINT ( 'NONE',  ( -27.50000000000000000, 15.87713240271474824, -15.54379906938135214 ) ) ;
#33588=VERTEX_POINT ( 'NONE', #23754 ) ;
#33599=MECHANICAL_DESIGN_GEOMETRIC_PRESENTATION_REPRESENTATION('',(#28149),#19457);
#33618=CARTESIAN_POINT ( 'NONE',  ( -27.50000000000000355, 0.000000000000000000, 0.000000000000000000 ) ) ;
#33621=CARTESIAN_POINT ( 'NONE',  ( -27.50000000000000000, 5.390523180938844305, -0.2837416352459747881 ) ) ;
#33635=CARTESIAN_POINT ( 'NONE',  ( 13.16654248868335664, -24.15255795529147065, -1.397731417911683705E-14 ) ) ;
#33673=DIRECTION ( 'NONE',  ( -0.000000000000000000, -0.000000000000000000, 1.000000000000000000 ) ) ;
#33685=EDGE_LOOP ( 'NONE', ( #3246, #17629, #23371, #18253 ) ) ;
ENDSEC;
END-ISO-10303-21;
